ISO-10303-21;
HEADER;
FILE_DESCRIPTION (('STEP AP214'),
    '1' );
FILE_NAME ('circlip for shafts normal_din_Circlip DIN 471 - 8 x 0.8.step',
    '2026-10-31T03:41:51',
    ( '' ),
    ( '' ),
    'SwSTEP 2.0',
    'SolidWorks 2026',
    '' );
FILE_SCHEMA (( 'AUTOMOTIVE_DESIGN' ));
ENDSEC;

DATA;
#10=ORIENTED_EDGE ( 'NONE', *, *, #14463, .T. ) ;
#13=ORIENTED_EDGE ( 'NONE', *, *, #14923, .F. ) ;
#25=LINE ( 'NONE', #3651, #6082 ) ;
#56=ORIENTED_EDGE ( 'NONE', *, *, #14923, .T. ) ;
#62=EDGE_CURVE ( 'NONE', #4667, #5041, #11487, .T. ) ;
#71=CARTESIAN_POINT ( 'NONE',  ( 2.321707774797442170, -4.824281976789052351, -0.8000000000000000444 ) ) ;
#88=ORIENTED_EDGE ( 'NONE', *, *, #2042, .F. ) ;
#93=AXIS2_PLACEMENT_3D ( 'NONE', #1649, #1959, #6645 ) ;
#105=DIRECTION ( 'NONE',  ( 1.000000000000000000, 0.000000000000000000, 0.000000000000000000 ) ) ;
#121=DIRECTION ( 'NONE',  ( 0.000000000000000000, 0.000000000000000000, 1.000000000000000000 ) ) ;
#131=PRESENTATION_STYLE_ASSIGNMENT (( #7148 ) ) ;
#156=CIRCLE ( 'NONE', #8761, 0.7500000000000002220 ) ;
#272=DIRECTION ( 'NONE',  ( 0.02857142857142857401, -0.9995917534020515305, 0.000000000000000000 ) ) ;
#275=LINE ( 'NONE', #354, #6695 ) ;
#280=CARTESIAN_POINT ( 'NONE',  ( 0.000000000000000000, 0.000000000000000000, -0.8000000000000000444 ) ) ;
#285=CARTESIAN_POINT ( 'NONE',  ( 0.1085714285714285687, -3.798448662927795372, 0.000000000000000000 ) ) ;
#348=VECTOR ( 'NONE', #6757, 1000.000000000000000 ) ;
#354=CARTESIAN_POINT ( 'NONE',  ( -1.000000000000000222, -4.808326913195983821, 0.000000000000000000 ) ) ;
#360=DIRECTION ( 'NONE',  ( -0.000000000000000000, -0.000000000000000000, -1.000000000000000000 ) ) ;
#403=AXIS2_PLACEMENT_3D ( 'NONE', #7843, #9071, #11364 ) ;
#421=ORIENTED_EDGE ( 'NONE', *, *, #8347, .F. ) ;
#427=LINE ( 'NONE', #11042, #5355 ) ;
#448=VERTEX_POINT ( 'NONE', #8125 ) ;
#479=DIRECTION ( 'NONE',  ( -0.9995917534020515305, -0.02857142857142857054, 0.000000000000000000 ) ) ;
#482=FACE_OUTER_BOUND ( 'NONE', #14654, .T. ) ;
#507=CARTESIAN_POINT ( 'NONE',  ( -3.799999999999999378, 4.653657836759941744E-16, -0.8000000000000000444 ) ) ;
#509=DIRECTION ( 'NONE',  ( 0.000000000000000000, 0.000000000000000000, 1.000000000000000000 ) ) ;
#513=ORIENTED_EDGE ( 'NONE', *, *, #4652, .F. ) ;
#517=ORIENTED_EDGE ( 'NONE', *, *, #5979, .F. ) ;
#568=ORIENTED_EDGE ( 'NONE', *, *, #11623, .T. ) ;
#574=EDGE_CURVE ( 'NONE', #4667, #7883, #12972, .T. ) ;
#594=DIRECTION ( 'NONE',  ( 0.000000000000000000, 0.000000000000000000, -1.000000000000000000 ) ) ;
#600=CARTESIAN_POINT ( 'NONE',  ( 0.000000000000000000, 0.000000000000000000, 0.000000000000000000 ) ) ;
#609=UNCERTAINTY_MEASURE_WITH_UNIT (LENGTH_MEASURE( 1.000000000000000082E-05 ), #10866, 'distance_accuracy_value', 'NONE');
#636=CARTESIAN_POINT ( 'NONE',  ( -0.1085714285714285687, -3.798448662927795372, -0.8000000000000000444 ) ) ;
#641=STYLED_ITEM ( 'NONE', ( #131 ), #675 ) ;
#651=EDGE_LOOP ( 'NONE', ( #7645, #7888, #4599, #10882 ) ) ;
#670=DIRECTION ( 'NONE',  ( 0.000000000000000000, 0.000000000000000000, 1.000000000000000000 ) ) ;
#675=ADVANCED_BREP_SHAPE_REPRESENTATION ( '', ( #14111, #1376 ), #3356 ) ;
#716=ADVANCED_FACE ( 'NONE', ( #4624 ), #4697, .F. ) ;
#721=CARTESIAN_POINT ( 'NONE',  ( -1.000000000000000000, -6.008326913195983998, -0.8000000000000000444 ) ) ;
#723=ORIENTED_EDGE ( 'NONE', *, *, #13418, .T. ) ;
#724=DIRECTION ( 'NONE',  ( 0.000000000000000000, 0.000000000000000000, 1.000000000000000000 ) ) ;
#727=ADVANCED_FACE ( 'NONE', ( #4841 ), #15146, .T. ) ;
#760=DIRECTION ( 'NONE',  ( 0.02857142857142857401, 0.9995917534020515305, -0.000000000000000000 ) ) ;
#797=VERTEX_POINT ( 'NONE', #2296 ) ;
#820=LINE ( 'NONE', #13660, #10113 ) ;
#836=CARTESIAN_POINT ( 'NONE',  ( -2.141980652367355020, -6.189445006155633422, 0.000000000000000000 ) ) ;
#837=DIRECTION ( 'NONE',  ( 0.000000000000000000, 0.000000000000000000, 1.000000000000000000 ) ) ;
#865=AXIS2_PLACEMENT_3D ( 'NONE', #4110, #8790, #13481 ) ;
#881=VECTOR ( 'NONE', #2943, 1000.000000000000000 ) ;
#914=EDGE_CURVE ( 'NONE', #9975, #4099, #3982, .T. ) ;
#921=CARTESIAN_POINT ( 'NONE',  ( 0.1717365941144614605, -6.008326913195983998, -0.8000000000000000444 ) ) ;
#932=EDGE_CURVE ( 'NONE', #12029, #4099, #5029, .T. ) ;
#933=DIRECTION ( 'NONE',  ( 0.000000000000000000, 0.000000000000000000, 1.000000000000000000 ) ) ;
#944=CIRCLE ( 'NONE', #2663, 0.7500000000000002220 ) ;
#951=CARTESIAN_POINT ( 'NONE',  ( 0.1999999999999985678, -6.997142273814360713, -0.8000000000000000444 ) ) ;
#953=DIRECTION ( 'NONE',  ( 1.000000000000000000, 0.000000000000000000, 0.000000000000000000 ) ) ;
#964=ORIENTED_EDGE ( 'NONE', *, *, #62, .F. ) ;
#1019=EDGE_CURVE ( 'NONE', #12415, #5464, #10648, .T. ) ;
#1030=AXIS2_PLACEMENT_3D ( 'NONE', #14428, #2890, #1737 ) ;
#1033=LINE ( 'NONE', #10334, #13131 ) ;
#1045=CYLINDRICAL_SURFACE ( 'NONE', #11953, 0.5999999999999998668 ) ;
#1067=DIRECTION ( 'NONE',  ( 0.000000000000000000, 0.000000000000000000, 1.000000000000000000 ) ) ;
#1070=EDGE_CURVE ( 'NONE', #13441, #8611, #4771, .T. ) ;
#1087=EDGE_LOOP ( 'NONE', ( #8142, #8059, #9530, #56 ) ) ;
#1117=ORIENTED_EDGE ( 'NONE', *, *, #12181, .F. ) ;
#1122=DIRECTION ( 'NONE',  ( 0.02857142857142857401, 0.9995917534020515305, -0.000000000000000000 ) ) ;
#1141=VECTOR ( 'NONE', #594, 1000.000000000000000 ) ;
#1145=CARTESIAN_POINT ( 'NONE',  ( 0.000000000000000000, 0.4273491293402468805, -0.8000000000000000444 ) ) ;
#1167=CARTESIAN_POINT ( 'NONE',  ( 1.000000000000000000, -4.808326913195983821, 0.000000000000000000 ) ) ;
#1201=CIRCLE ( 'NONE', #2400, 0.5999999999999999778 ) ;
#1229=DIRECTION ( 'NONE',  ( 0.000000000000000000, 0.000000000000000000, 1.000000000000000000 ) ) ;
#1254=EDGE_CURVE ( 'NONE', #10971, #5354, #13309, .T. ) ;
#1272=CARTESIAN_POINT ( 'NONE',  ( 0.000000000000000000, 0.000000000000000000, 0.000000000000000000 ) ) ;
#1278=VERTEX_POINT ( 'NONE', #7480 ) ;
#1293=PLANE ( 'NONE',  #8047 ) ;
#1324=DIRECTION ( 'NONE',  ( 0.000000000000000000, 0.000000000000000000, 1.000000000000000000 ) ) ;
#1327=AXIS2_PLACEMENT_3D ( 'NONE', #8141, #12532, #6625 ) ;
#1365=CARTESIAN_POINT ( 'NONE',  ( 0.9999999999999997780, -6.008326913195983998, -0.8000000000000000444 ) ) ;
#1374=CIRCLE ( 'NONE', #2365, 2.447112362156698140 ) ;
#1375=ORIENTED_EDGE ( 'NONE', *, *, #4711, .T. ) ;
#1376=AXIS2_PLACEMENT_3D ( 'NONE', #7353, #6187, #9640 ) ;
#1389=AXIS2_PLACEMENT_3D ( 'NONE', #636, #4027, #8788 ) ;
#1462=ORIENTED_EDGE ( 'NONE', *, *, #4915, .T. ) ;
#1480=FACE_OUTER_BOUND ( 'NONE', #4378, .T. ) ;
#1496=CYLINDRICAL_SURFACE ( 'NONE', #8697, 4.872650870659752442 ) ;
#1520=CARTESIAN_POINT ( 'NONE',  ( -2.321707774797442170, -4.824281976789052351, -0.8000000000000000444 ) ) ;
#1522=ORIENTED_EDGE ( 'NONE', *, *, #12181, .T. ) ;
#1534=CARTESIAN_POINT ( 'NONE',  ( 0.9999999999999997780, -6.008326913195983998, -0.8000000000000000444 ) ) ;
#1567=( NAMED_UNIT ( * ) PLANE_ANGLE_UNIT ( ) SI_UNIT ( $, .RADIAN. ) );
#1577=VERTEX_POINT ( 'NONE', #3538 ) ;
#1620=DIRECTION ( 'NONE',  ( 1.000000000000000000, 0.000000000000000000, 0.000000000000000000 ) ) ;
#1649=CARTESIAN_POINT ( 'NONE',  ( 1.000000000000000000, -5.408326913195983465, -0.8000000000000000444 ) ) ;
#1687=ORIENTED_EDGE ( 'NONE', *, *, #4711, .F. ) ;
#1695=CARTESIAN_POINT ( 'NONE',  ( 0.000000000000000000, 0.000000000000000000, -0.8000000000000000444 ) ) ;
#1702=ORIENTED_EDGE ( 'NONE', *, *, #7697, .F. ) ;
#1724=VERTEX_POINT ( 'NONE', #7621 ) ;
#1726=DIRECTION ( 'NONE',  ( 0.000000000000000000, 0.000000000000000000, 1.000000000000000000 ) ) ;
#1729=( NAMED_UNIT ( * ) SI_UNIT ( $, .STERADIAN. ) SOLID_ANGLE_UNIT ( ) );
#1737=DIRECTION ( 'NONE',  ( 0.000000000000000000, -0.000000000000000000, 1.000000000000000000 ) ) ;
#1747=DIRECTION ( 'NONE',  ( 0.000000000000000000, 0.000000000000000000, 1.000000000000000000 ) ) ;
#1781=DIRECTION ( 'NONE',  ( 1.000000000000000000, 0.000000000000000000, 0.000000000000000000 ) ) ;
#1782=EDGE_CURVE ( 'NONE', #1577, #10971, #9148, .T. ) ;
#1785=PRODUCT_DEFINITION_CONTEXT ( 'detailed design', #3121, 'design' ) ;
#1787=DIRECTION ( 'NONE',  ( 0.02857142857142857401, 0.9995917534020515305, -0.000000000000000000 ) ) ;
#1789=CARTESIAN_POINT ( 'NONE',  ( 0.9999999999999997780, -6.008326913195983998, 0.000000000000000000 ) ) ;
#1815=CYLINDRICAL_SURFACE ( 'NONE', #4126, 0.5999999999999999778 ) ;
#1824=FACE_OUTER_BOUND ( 'NONE', #11913, .T. ) ;
#1836=ORIENTED_EDGE ( 'NONE', *, *, #9897, .T. ) ;
#1839=DIRECTION ( 'NONE',  ( 0.000000000000000000, 0.000000000000000000, 1.000000000000000000 ) ) ;
#1843=CARTESIAN_POINT ( 'NONE',  ( 0.1085714285714285687, -3.798448662927795372, -0.8000000000000000444 ) ) ;
#1853=VECTOR ( 'NONE', #11773, 1000.000000000000000 ) ;
#1876=PLANE ( 'NONE',  #1389 ) ;
#1906=VECTOR ( 'NONE', #8668, 1000.000000000000000 ) ;
#1907=DIRECTION ( 'NONE',  ( 0.000000000000000000, 0.000000000000000000, 1.000000000000000000 ) ) ;
#1908=DIRECTION ( 'NONE',  ( 0.000000000000000000, 0.000000000000000000, 1.000000000000000000 ) ) ;
#1927=FACE_OUTER_BOUND ( 'NONE', #9836, .T. ) ;
#1931=EDGE_CURVE ( 'NONE', #12415, #7949, #2462, .T. ) ;
#1959=DIRECTION ( 'NONE',  ( 0.000000000000000000, 0.000000000000000000, 1.000000000000000000 ) ) ;
#1966=VECTOR ( 'NONE', #13841, 1000.000000000000000 ) ;
#1980=CARTESIAN_POINT ( 'NONE',  ( 0.000000000000000000, 0.4273491293402468805, 0.000000000000000000 ) ) ;
#2003=LINE ( 'NONE', #6686, #9194 ) ;
#2028=CIRCLE ( 'NONE', #10620, 3.799999999999999378 ) ;
#2042=EDGE_CURVE ( 'NONE', #4474, #8109, #10464, .T. ) ;
#2058=ORIENTED_EDGE ( 'NONE', *, *, #12577, .T. ) ;
#2081=EDGE_LOOP ( 'NONE', ( #12736, #9559, #6883, #9632 ) ) ;
#2120=VECTOR ( 'NONE', #11371, 1000.000000000000000 ) ;
#2192=EDGE_CURVE ( 'NONE', #5464, #448, #820, .T. ) ;
#2195=VERTEX_POINT ( 'NONE', #3144 ) ;
#2196=DIRECTION ( 'NONE',  ( 0.000000000000000000, 0.000000000000000000, -1.000000000000000000 ) ) ;
#2214=AXIS2_PLACEMENT_3D ( 'NONE', #3057, #670, #12646 ) ;
#2239=DIRECTION ( 'NONE',  ( 1.000000000000000000, 0.000000000000000000, 0.000000000000000000 ) ) ;
#2244=FACE_OUTER_BOUND ( 'NONE', #14397, .T. ) ;
#2260=VECTOR ( 'NONE', #7431, 1000.000000000000000 ) ;
#2269=CIRCLE ( 'NONE', #12323, 0.5999999999999998668 ) ;
#2278=CARTESIAN_POINT ( 'NONE',  ( 1.599999999999999867, -5.408326913195983465, 0.000000000000000000 ) ) ;
#2296=CARTESIAN_POINT ( 'NONE',  ( 1.599999999999999867, -5.408326913195983465, -0.8000000000000000444 ) ) ;
#2310=CYLINDRICAL_SURFACE ( 'NONE', #12232, 7.000000000000000000 ) ;
#2322=ORIENTED_EDGE ( 'NONE', *, *, #1019, .F. ) ;
#2326=ORIENTED_EDGE ( 'NONE', *, *, #12496, .F. ) ;
#2359=VERTEX_POINT ( 'NONE', #8267 ) ;
#2365=AXIS2_PLACEMENT_3D ( 'NONE', #14254, #13975, #4962 ) ;
#2372=DIRECTION ( 'NONE',  ( 1.000000000000000000, 0.000000000000000000, 0.000000000000000000 ) ) ;
#2382=( NAMED_UNIT ( * ) SI_UNIT ( $, .STERADIAN. ) SOLID_ANGLE_UNIT ( ) );
#2392=EDGE_CURVE ( 'NONE', #7949, #448, #8877, .T. ) ;
#2398=VECTOR ( 'NONE', #13030, 1000.000000000000000 ) ;
#2400=AXIS2_PLACEMENT_3D ( 'NONE', #11777, #3556, #953 ) ;
#2409=EDGE_CURVE ( 'NONE', #5354, #6094, #8376, .T. ) ;
#2440=DIRECTION ( 'NONE',  ( 0.000000000000000000, 0.000000000000000000, 1.000000000000000000 ) ) ;
#2462=LINE ( 'NONE', #11816, #4829 ) ;
#2465=SURFACE_SIDE_STYLE ('',( #10677 ) ) ;
#2484=ORIENTED_EDGE ( 'NONE', *, *, #932, .T. ) ;
#2499=ADVANCED_FACE ( 'NONE', ( #2740 ), #13092, .F. ) ;
#2526=EDGE_CURVE ( 'NONE', #2359, #3152, #13260, .T. ) ;
#2541=CARTESIAN_POINT ( 'NONE',  ( 0.000000000000000000, 0.000000000000000000, 0.000000000000000000 ) ) ;
#2547=PLANE ( 'NONE',  #6503 ) ;
#2556=CIRCLE ( 'NONE', #9685, 4.872650870659752442 ) ;
#2564=ORIENTED_EDGE ( 'NONE', *, *, #14781, .F. ) ;
#2566=ORIENTED_EDGE ( 'NONE', *, *, #4687, .F. ) ;
#2612=ORIENTED_EDGE ( 'NONE', *, *, #8379, .F. ) ;
#2639=AXIS2_PLACEMENT_3D ( 'NONE', #6529, #6449, #3072 ) ;
#2648=EDGE_LOOP ( 'NONE', ( #10925, #11074, #517, #8122 ) ) ;
#2661=EDGE_CURVE ( 'NONE', #5872, #10328, #6721, .T. ) ;
#2663=AXIS2_PLACEMENT_3D ( 'NONE', #4672, #12787, #11936 ) ;
#2730=DIRECTION ( 'NONE',  ( 1.000000000000000000, 0.000000000000000000, 0.000000000000000000 ) ) ;
#2732=EDGE_LOOP ( 'NONE', ( #10242, #9798, #5877, #6411 ) ) ;
#2740=FACE_OUTER_BOUND ( 'NONE', #10000, .T. ) ;
#2803=VECTOR ( 'NONE', #1324, 1000.000000000000000 ) ;
#2806=EDGE_LOOP ( 'NONE', ( #13025, #13263, #13186, #723 ) ) ;
#2816=CIRCLE ( 'NONE', #93, 0.5999999999999998668 ) ;
#2823=DIRECTION ( 'NONE',  ( 0.1305261922200521840, -0.9914448613738103822, 0.000000000000000000 ) ) ;
#2837=EDGE_LOOP ( 'NONE', ( #14020, #12866, #11290, #13398 ) ) ;
#2864=ORIENTED_EDGE ( 'NONE', *, *, #10013, .F. ) ;
#2890=DIRECTION ( 'NONE',  ( -0.000000000000000000, 1.000000000000000000, 0.000000000000000000 ) ) ;
#2943=DIRECTION ( 'NONE',  ( -0.000000000000000000, -0.000000000000000000, 1.000000000000000000 ) ) ;
#2953=CARTESIAN_POINT ( 'NONE',  ( 0.1085714285714285687, -3.798448662927795372, -0.8000000000000000444 ) ) ;
#2954=PRODUCT_DEFINITION_SHAPE ( 'NONE', 'NONE',  #12277 ) ;
#2956=ORIENTED_EDGE ( 'NONE', *, *, #14767, .T. ) ;
#2957=VERTEX_POINT ( 'NONE', #3708 ) ;
#2997=DIRECTION ( 'NONE',  ( -1.000000000000000000, -0.000000000000000000, -0.000000000000000000 ) ) ;
#3005=ORIENTED_EDGE ( 'NONE', *, *, #2409, .F. ) ;
#3015=UNCERTAINTY_MEASURE_WITH_UNIT (LENGTH_MEASURE( 1.000000000000000082E-05 ), #3755, 'distance_accuracy_value', 'NONE');
#3057=CARTESIAN_POINT ( 'NONE',  ( -1.000000000000000000, -5.408326913195983465, -0.8000000000000000444 ) ) ;
#3072=DIRECTION ( 'NONE',  ( 1.000000000000000000, 0.000000000000000000, 0.000000000000000000 ) ) ;
#3094=DIRECTION ( 'NONE',  ( 1.000000000000000000, 0.000000000000000000, 0.000000000000000000 ) ) ;
#3121=APPLICATION_CONTEXT ( 'automotive_design' ) ;
#3127=AXIS2_PLACEMENT_3D ( 'NONE', #8280, #9361, #14279 ) ;
#3133=EDGE_CURVE ( 'NONE', #7072, #9975, #11387, .T. ) ;
#3144=CARTESIAN_POINT ( 'NONE',  ( -0.1717365941144614327, -6.008326913195983998, -0.8000000000000000444 ) ) ;
#3152=VERTEX_POINT ( 'NONE', #11523 ) ;
#3187=AXIS2_PLACEMENT_3D ( 'NONE', #2541, #8225, #3616 ) ;
#3212=DIRECTION ( 'NONE',  ( 0.000000000000000000, 0.000000000000000000, 1.000000000000000000 ) ) ;
#3216=CARTESIAN_POINT ( 'NONE',  ( 0.000000000000000000, 0.000000000000000000, -0.8000000000000000444 ) ) ;
#3251=CARTESIAN_POINT ( 'NONE',  ( -1.000000000000000222, -4.808326913195983821, -0.8000000000000000444 ) ) ;
#3259=EDGE_CURVE ( 'NONE', #12986, #1724, #4294, .T. ) ;
#3274=EDGE_CURVE ( 'NONE', #797, #6094, #4929, .T. ) ;
#3277=DIRECTION ( 'NONE',  ( -0.9995917534020515305, -0.02857142857142857054, 0.000000000000000000 ) ) ;
#3299=DIRECTION ( 'NONE',  ( -0.9914448613738103822, -0.1305261922200521840, 0.000000000000000000 ) ) ;
#3344=CARTESIAN_POINT ( 'NONE',  ( 3.799999999999999378, 0.000000000000000000, -0.8000000000000000444 ) ) ;
#3356=( GEOMETRIC_REPRESENTATION_CONTEXT ( 3 ) GLOBAL_UNCERTAINTY_ASSIGNED_CONTEXT ( ( #6240 ) ) GLOBAL_UNIT_ASSIGNED_CONTEXT ( ( #13124, #12892, #2382 ) ) REPRESENTATION_CONTEXT ( 'NONE', 'WORKASPACE' ) );
#3378=CARTESIAN_POINT ( 'NONE',  ( 0.000000000000000000, 0.4273491293402468805, -0.8000000000000000444 ) ) ;
#3395=FACE_OUTER_BOUND ( 'NONE', #2081, .T. ) ;
#3441=CARTESIAN_POINT ( 'NONE',  ( -1.566204647097437563, -6.822536405429463713, -0.8000000000000000444 ) ) ;
#3459=( NAMED_UNIT ( * ) SI_UNIT ( $, .STERADIAN. ) SOLID_ANGLE_UNIT ( ) );
#3466=CARTESIAN_POINT ( 'NONE',  ( 0.000000000000000000, 0.000000000000000000, -0.8000000000000000444 ) ) ;
#3500=CARTESIAN_POINT ( 'NONE',  ( -1.000000000000000222, -4.808326913195983821, -0.8000000000000000444 ) ) ;
#3538=CARTESIAN_POINT ( 'NONE',  ( 0.1717365941144614327, -6.008326913195983998, -0.8000000000000000444 ) ) ;
#3545=ORIENTED_EDGE ( 'NONE', *, *, #8613, .F. ) ;
#3549=ORIENTED_EDGE ( 'NONE', *, *, #6748, .F. ) ;
#3553=ORIENTED_EDGE ( 'NONE', *, *, #12496, .T. ) ;
#3556=DIRECTION ( 'NONE',  ( 0.000000000000000000, 0.000000000000000000, 1.000000000000000000 ) ) ;
#3577=VECTOR ( 'NONE', #1787, 1000.000000000000114 ) ;
#3593=LINE ( 'NONE', #8283, #10375 ) ;
#3616=DIRECTION ( 'NONE',  ( 1.000000000000000000, 0.000000000000000000, 0.000000000000000000 ) ) ;
#3639=VECTOR ( 'NONE', #5430, 1000.000000000000000 ) ;
#3642=PLANE ( 'NONE',  #6807 ) ;
#3647=EDGE_CURVE ( 'NONE', #8611, #10625, #12186, .T. ) ;
#3649=CARTESIAN_POINT ( 'NONE',  ( 0.000000000000000000, 0.4273491293402468805, 0.000000000000000000 ) ) ;
#3651=CARTESIAN_POINT ( 'NONE',  ( -0.1085714285714285687, -3.798448662927795372, -0.8000000000000000444 ) ) ;
#3664=VERTEX_POINT ( 'NONE', #10651 ) ;
#3670=CARTESIAN_POINT ( 'NONE',  ( 1.398397006336996817, -6.091550361990593743, 0.000000000000000000 ) ) ;
#3707=DIRECTION ( 'NONE',  ( -1.000000000000000000, 0.000000000000000000, 0.000000000000000000 ) ) ;
#3708=CARTESIAN_POINT ( 'NONE',  ( -3.160591952521660364, -3.281206521718067037, -0.8000000000000000444 ) ) ;
#3715=EDGE_CURVE ( 'NONE', #8611, #5631, #12334, .T. ) ;
#3755=( LENGTH_UNIT ( ) NAMED_UNIT ( * ) SI_UNIT ( .MILLI., .METRE. ) );
#3769=ORIENTED_EDGE ( 'NONE', *, *, #3274, .F. ) ;
#3771=DIRECTION ( 'NONE',  ( 0.9914448613738103822, -0.1305261922200521840, 0.000000000000000000 ) ) ;
#3774=VECTOR ( 'NONE', #14090, 1000.000000000000000 ) ;
#3775=ORIENTED_EDGE ( 'NONE', *, *, #12835, .T. ) ;
#3777=AXIS2_PLACEMENT_3D ( 'NONE', #14750, #1908, #13579 ) ;
#3839=ORIENTED_EDGE ( 'NONE', *, *, #11668, .F. ) ;
#3867=CARTESIAN_POINT ( 'NONE',  ( -0.1085714285714285687, -3.798448662927795372, 0.000000000000000000 ) ) ;
#3916=DIRECTION ( 'NONE',  ( 1.000000000000000000, 0.000000000000000000, 0.000000000000000000 ) ) ;
#3926=DIRECTION ( 'NONE',  ( 0.000000000000000000, 0.000000000000000000, 1.000000000000000000 ) ) ;
#3927=LINE ( 'NONE', #1534, #1906 ) ;
#3934=CARTESIAN_POINT ( 'NONE',  ( -0.2000000000000000111, -6.997142273814360713, -0.8000000000000000444 ) ) ;
#3953=CARTESIAN_POINT ( 'NONE',  ( 1.398397006336996817, -6.091550361990593743, -0.8000000000000000444 ) ) ;
#3982=LINE ( 'NONE', #507, #5759 ) ;
#3989=VERTEX_POINT ( 'NONE', #12851 ) ;
#3990=ADVANCED_FACE ( 'NONE', ( #10567 ), #3642, .F. ) ;
#4017=DIRECTION ( 'NONE',  ( 1.000000000000000000, -0.000000000000000000, -0.000000000000000000 ) ) ;
#4027=DIRECTION ( 'NONE',  ( 0.9995917534020515305, -0.02857142857142857054, 0.000000000000000000 ) ) ;
#4058=LINE ( 'NONE', #5071, #14048 ) ;
#4060=DIRECTION ( 'NONE',  ( 0.000000000000000000, 0.000000000000000000, 1.000000000000000000 ) ) ;
#4091=AXIS2_PLACEMENT_3D ( 'NONE', #5161, #360, #3916 ) ;
#4099=VERTEX_POINT ( 'NONE', #13391 ) ;
#4108=AXIS2_PLACEMENT_3D ( 'NONE', #3378, #13754, #11586 ) ;
#4110=CARTESIAN_POINT ( 'NONE',  ( -1.398397006336996817, -6.091550361990593743, -0.8000000000000000444 ) ) ;
#4126=AXIS2_PLACEMENT_3D ( 'NONE', #9819, #13504, #14514 ) ;
#4146=ADVANCED_FACE ( 'NONE', ( #13314 ), #7488, .T. ) ;
#4157=CARTESIAN_POINT ( 'NONE',  ( 2.141980652367355464, -6.189445006155633422, -0.8000000000000000444 ) ) ;
#4173=ORIENTED_EDGE ( 'NONE', *, *, #9950, .F. ) ;
#4188=CARTESIAN_POINT ( 'NONE',  ( 0.1085714285714285687, -3.798448662927795372, 0.000000000000000000 ) ) ;
#4213=CARTESIAN_POINT ( 'NONE',  ( 0.1717365941144614327, -6.008326913195983998, 0.000000000000000000 ) ) ;
#4261=CARTESIAN_POINT ( 'NONE',  ( 4.872650870659752442, 0.4273491293402468805, -0.8000000000000000444 ) ) ;
#4291=ORIENTED_EDGE ( 'NONE', *, *, #1019, .T. ) ;
#4294=CIRCLE ( 'NONE', #8210, 7.000000000000000000 ) ;
#4303=CARTESIAN_POINT ( 'NONE',  ( -4.872650870659752442, 0.4273491293402474911, -0.8000000000000000444 ) ) ;
#4318=ORIENTED_EDGE ( 'NONE', *, *, #5219, .F. ) ;
#4346=EDGE_LOOP ( 'NONE', ( #10185, #5775, #13523, #5231 ) ) ;
#4368=DIRECTION ( 'NONE',  ( -0.000000000000000000, -0.000000000000000000, 1.000000000000000000 ) ) ;
#4378=EDGE_LOOP ( 'NONE', ( #4173, #2612, #4730, #11268 ) ) ;
#4411=LINE ( 'NONE', #10240, #1966 ) ;
#4428=VECTOR ( 'NONE', #4368, 1000.000000000000000 ) ;
#4437=ORIENTED_EDGE ( 'NONE', *, *, #14756, .F. ) ;
#4474=VERTEX_POINT ( 'NONE', #6534 ) ;
#4510=CARTESIAN_POINT ( 'NONE',  ( 1.000000000000000000, -5.408326913195983465, -0.8000000000000000444 ) ) ;
#4526=VERTEX_POINT ( 'NONE', #9516 ) ;
#4564=ORIENTED_EDGE ( 'NONE', *, *, #1070, .F. ) ;
#4568=ORIENTED_EDGE ( 'NONE', *, *, #6748, .T. ) ;
#4574=EDGE_CURVE ( 'NONE', #6094, #5377, #2269, .T. ) ;
#4599=ORIENTED_EDGE ( 'NONE', *, *, #9349, .T. ) ;
#4617=VERTEX_POINT ( 'NONE', #9363 ) ;
#4624=FACE_OUTER_BOUND ( 'NONE', #10284, .T. ) ;
#4640=DIRECTION ( 'NONE',  ( 0.000000000000000000, 0.000000000000000000, 1.000000000000000000 ) ) ;
#4652=EDGE_CURVE ( 'NONE', #6129, #15110, #3593, .T. ) ;
#4667=VERTEX_POINT ( 'NONE', #7288 ) ;
#4668=EDGE_CURVE ( 'NONE', #8109, #10680, #9823, .T. ) ;
#4672=CARTESIAN_POINT ( 'NONE',  ( -1.398397006336996817, -6.091550361990593743, 0.000000000000000000 ) ) ;
#4682=AXIS2_PLACEMENT_3D ( 'NONE', #1365, #11591, #5764 ) ;
#4687=EDGE_CURVE ( 'NONE', #9975, #4667, #2028, .T. ) ;
#4695=EDGE_CURVE ( 'NONE', #9070, #3664, #4058, .T. ) ;
#4697=PLANE ( 'NONE',  #11504 ) ;
#4711=EDGE_CURVE ( 'NONE', #14392, #15110, #275, .T. ) ;
#4730=ORIENTED_EDGE ( 'NONE', *, *, #8613, .T. ) ;
#4744=ORIENTED_EDGE ( 'NONE', *, *, #12577, .F. ) ;
#4750=EDGE_LOOP ( 'NONE', ( #3769, #8499, #7695, #9815 ) ) ;
#4755=CARTESIAN_POINT ( 'NONE',  ( 1.566204647097437341, -6.822536405429464601, -0.8000000000000000444 ) ) ;
#4756=CARTESIAN_POINT ( 'NONE',  ( 0.1085714285714285687, -3.798448662927795372, 0.000000000000000000 ) ) ;
#4770=FILL_AREA_STYLE_COLOUR ( '', #5340 ) ;
#4771=CIRCLE ( 'NONE', #8676, 4.872650870659752442 ) ;
#4829=VECTOR ( 'NONE', #1229, 1000.000000000000000 ) ;
#4839=ORIENTED_EDGE ( 'NONE', *, *, #8625, .F. ) ;
#4841=FACE_OUTER_BOUND ( 'NONE', #2732, .T. ) ;
#4843=CARTESIAN_POINT ( 'NONE',  ( -0.1085714285714285687, -3.798448662927795372, -0.8000000000000000444 ) ) ;
#4880=ORIENTED_EDGE ( 'NONE', *, *, #11693, .T. ) ;
#4915=EDGE_CURVE ( 'NONE', #1577, #8659, #5960, .T. ) ;
#4919=DIRECTION ( 'NONE',  ( -1.000000000000000000, 0.000000000000000000, 0.000000000000000000 ) ) ;
#4929=LINE ( 'NONE', #12974, #348 ) ;
#4931=ORIENTED_EDGE ( 'NONE', *, *, #7955, .F. ) ;
#4962=DIRECTION ( 'NONE',  ( 1.000000000000000000, 0.000000000000000000, 0.000000000000000000 ) ) ;
#4987=APPLICATION_CONTEXT ( 'automotive_design' ) ;
#5029=CIRCLE ( 'NONE', #9183, 3.799999999999999378 ) ;
#5031=ORIENTED_EDGE ( 'NONE', *, *, #10245, .T. ) ;
#5041=VERTEX_POINT ( 'NONE', #11642 ) ;
#5057=DIRECTION ( 'NONE',  ( 1.000000000000000000, 0.000000000000000000, 0.000000000000000000 ) ) ;
#5071=CARTESIAN_POINT ( 'NONE',  ( 0.9999999999999997780, -6.008326913195983998, 0.000000000000000000 ) ) ;
#5124=VECTOR ( 'NONE', #6065, 1000.000000000000000 ) ;
#5161=CARTESIAN_POINT ( 'NONE',  ( -4.747884751462026820, -5.143694235355983579, 0.000000000000000000 ) ) ;
#5171=CARTESIAN_POINT ( 'NONE',  ( 3.160591952521659032, -3.281206521718069258, -0.8000000000000000444 ) ) ;
#5186=FACE_OUTER_BOUND ( 'NONE', #8298, .T. ) ;
#5188=EDGE_LOOP ( 'NONE', ( #8642, #10229, #2864, #12517 ) ) ;
#5219=EDGE_CURVE ( 'NONE', #5377, #8463, #4411, .T. ) ;
#5231=ORIENTED_EDGE ( 'NONE', *, *, #4915, .F. ) ;
#5237=DIRECTION ( 'NONE',  ( 1.000000000000000000, 0.000000000000000000, 0.000000000000000000 ) ) ;
#5287=CARTESIAN_POINT ( 'NONE',  ( 2.321707774797442170, -4.824281976789052351, -0.8000000000000000444 ) ) ;
#5288=ORIENTED_EDGE ( 'NONE', *, *, #15201, .F. ) ;
#5340=COLOUR_RGB ( '',1.000000000000000000, 0.9490196078431372140, 0.9098039215686274384 ) ;
#5354=VERTEX_POINT ( 'NONE', #10615 ) ;
#5355=VECTOR ( 'NONE', #1747, 1000.000000000000000 ) ;
#5361=CARTESIAN_POINT ( 'NONE',  ( -2.321707774797442170, -4.824281976789052351, -0.8000000000000000444 ) ) ;
#5377=VERTEX_POINT ( 'NONE', #1167 ) ;
#5389=EDGE_CURVE ( 'NONE', #5041, #12602, #12515, .T. ) ;
#5430=DIRECTION ( 'NONE',  ( 0.000000000000000000, 0.000000000000000000, 1.000000000000000000 ) ) ;
#5446=DIRECTION ( 'NONE',  ( 0.000000000000000000, 0.000000000000000000, 1.000000000000000000 ) ) ;
#5464=VERTEX_POINT ( 'NONE', #3934 ) ;
#5484=CYLINDRICAL_SURFACE ( 'NONE', #11459, 3.799999999999999378 ) ;
#5485=CYLINDRICAL_SURFACE ( 'NONE', #8075, 0.5999999999999998668 ) ;
#5495=ORIENTED_EDGE ( 'NONE', *, *, #2392, .T. ) ;
#5541=DIRECTION ( 'NONE',  ( 0.000000000000000000, 0.000000000000000000, 1.000000000000000000 ) ) ;
#5545=CIRCLE ( 'NONE', #865, 0.7500000000000002220 ) ;
#5546=CARTESIAN_POINT ( 'NONE',  ( 3.160591952521659032, -3.281206521718069258, 0.000000000000000000 ) ) ;
#5605=CYLINDRICAL_SURFACE ( 'NONE', #12958, 3.799999999999999378 ) ;
#5629=VERTEX_POINT ( 'NONE', #5546 ) ;
#5631=VERTEX_POINT ( 'NONE', #10219 ) ;
#5664=DIRECTION ( 'NONE',  ( 0.000000000000000000, 0.000000000000000000, 1.000000000000000000 ) ) ;
#5670=DIRECTION ( 'NONE',  ( 0.02857142857142857054, -0.9995917534020515305, 0.000000000000000000 ) ) ;
#5689=FACE_OUTER_BOUND ( 'NONE', #14024, .T. ) ;
#5715=ADVANCED_FACE ( 'NONE', ( #11661 ), #10665, .F. ) ;
#5724=EDGE_CURVE ( 'NONE', #13441, #5629, #5845, .T. ) ;
#5752=AXIS2_PLACEMENT_3D ( 'NONE', #3953, #7563, #3707 ) ;
#5759=VECTOR ( 'NONE', #4060, 1000.000000000000000 ) ;
#5764=DIRECTION ( 'NONE',  ( 0.000000000000000000, 0.000000000000000000, -1.000000000000000000 ) ) ;
#5775=ORIENTED_EDGE ( 'NONE', *, *, #1254, .T. ) ;
#5783=CARTESIAN_POINT ( 'NONE',  ( 0.000000000000000000, 0.000000000000000000, -0.8000000000000000444 ) ) ;
#5830=CARTESIAN_POINT ( 'NONE',  ( 1.000000000000000000, -5.408326913195983465, 0.000000000000000000 ) ) ;
#5837=ORIENTED_EDGE ( 'NONE', *, *, #5724, .T. ) ;
#5842=CIRCLE ( 'NONE', #6805, 7.000000000000000000 ) ;
#5845=LINE ( 'NONE', #6062, #14236 ) ;
#5850=DIRECTION ( 'NONE',  ( 1.000000000000000000, 0.000000000000000000, 0.000000000000000000 ) ) ;
#5872=VERTEX_POINT ( 'NONE', #1520 ) ;
#5877=ORIENTED_EDGE ( 'NONE', *, *, #9897, .F. ) ;
#5879=CARTESIAN_POINT ( 'NONE',  ( 2.321707774797442170, -4.824281976789052351, 0.000000000000000000 ) ) ;
#5881=CARTESIAN_POINT ( 'NONE',  ( 0.000000000000000000, 0.4273491293402468805, -0.8000000000000000444 ) ) ;
#5892=AXIS2_PLACEMENT_3D ( 'NONE', #3216, #1907, #7666 ) ;
#5913=LINE ( 'NONE', #4755, #2398 ) ;
#5921=ORIENTED_EDGE ( 'NONE', *, *, #10686, .T. ) ;
#5960=LINE ( 'NONE', #10506, #7834 ) ;
#5965=DIRECTION ( 'NONE',  ( 1.000000000000000000, 0.000000000000000000, 0.000000000000000000 ) ) ;
#5977=DIRECTION ( 'NONE',  ( -0.000000000000000000, -0.000000000000000000, 1.000000000000000000 ) ) ;
#5978=ADVANCED_FACE ( 'NONE', ( #1824 ), #8885, .F. ) ;
#5979=EDGE_CURVE ( 'NONE', #6129, #1278, #9814, .T. ) ;
#5981=DIRECTION ( 'NONE',  ( 0.000000000000000000, -0.000000000000000000, 1.000000000000000000 ) ) ;
#5984=CARTESIAN_POINT ( 'NONE',  ( 2.321707774797442170, -4.824281976789052351, 0.000000000000000000 ) ) ;
#6019=DIRECTION ( 'NONE',  ( 1.000000000000000000, 0.000000000000000000, 0.000000000000000000 ) ) ;
#6055=EDGE_CURVE ( 'NONE', #8659, #5354, #10199, .T. ) ;
#6062=CARTESIAN_POINT ( 'NONE',  ( 3.160591952521659032, -3.281206521718069258, -0.8000000000000000444 ) ) ;
#6065=DIRECTION ( 'NONE',  ( -1.000000000000000000, -0.000000000000000000, -0.000000000000000000 ) ) ;
#6082=VECTOR ( 'NONE', #1122, 1000.000000000000114 ) ;
#6094=VERTEX_POINT ( 'NONE', #2278 ) ;
#6095=AXIS2_PLACEMENT_3D ( 'NONE', #280, #509, #10972 ) ;
#6117=DIRECTION ( 'NONE',  ( 1.000000000000000000, 0.000000000000000000, -0.000000000000000000 ) ) ;
#6129=VERTEX_POINT ( 'NONE', #3500 ) ;
#6136=DIRECTION ( 'NONE',  ( 1.000000000000000000, 0.000000000000000000, 0.000000000000000000 ) ) ;
#6145=ORIENTED_EDGE ( 'NONE', *, *, #3133, .F. ) ;
#6187=DIRECTION ( 'NONE',  ( 0.000000000000000000, 0.000000000000000000, 1.000000000000000000 ) ) ;
#6240=UNCERTAINTY_MEASURE_WITH_UNIT (LENGTH_MEASURE( 1.000000000000000082E-05 ), #13124, 'distance_accuracy_value', 'NONE');
#6266=ORIENTED_EDGE ( 'NONE', *, *, #4668, .F. ) ;
#6333=AXIS2_PLACEMENT_3D ( 'NONE', #9046, #5446, #14974 ) ;
#6361=PRODUCT_CONTEXT ( 'NONE', #4987, 'mechanical' ) ;
#6379=CARTESIAN_POINT ( 'NONE',  ( -0.1374368770859597522, -4.808326913195983821, 0.000000000000000000 ) ) ;
#6411=ORIENTED_EDGE ( 'NONE', *, *, #5724, .F. ) ;
#6444=LINE ( 'NONE', #11121, #1141 ) ;
#6449=DIRECTION ( 'NONE',  ( 0.000000000000000000, 0.000000000000000000, 1.000000000000000000 ) ) ;
#6468=EDGE_CURVE ( 'NONE', #15110, #9070, #1201, .T. ) ;
#6487=DIRECTION ( 'NONE',  ( 1.000000000000000000, 0.000000000000000000, 0.000000000000000000 ) ) ;
#6503=AXIS2_PLACEMENT_3D ( 'NONE', #71, #3771, #9464 ) ;
#6515=ORIENTED_EDGE ( 'NONE', *, *, #4668, .T. ) ;
#6529=CARTESIAN_POINT ( 'NONE',  ( 1.000000000000000000, -5.408326913195983465, -0.8000000000000000444 ) ) ;
#6534=CARTESIAN_POINT ( 'NONE',  ( -3.160591952521660364, -3.281206521718067037, 0.000000000000000000 ) ) ;
#6574=VERTEX_POINT ( 'NONE', #6876 ) ;
#6601=ORIENTED_EDGE ( 'NONE', *, *, #8347, .T. ) ;
#6609=CARTESIAN_POINT ( 'NONE',  ( -0.1085714285714285687, -3.798448662927795372, 0.000000000000000000 ) ) ;
#6617=PLANE ( 'NONE',  #13860 ) ;
#6625=DIRECTION ( 'NONE',  ( 1.000000000000000000, 0.000000000000000000, 0.000000000000000000 ) ) ;
#6637=DIRECTION ( 'NONE',  ( 1.000000000000000000, 0.000000000000000000, 0.000000000000000000 ) ) ;
#6645=DIRECTION ( 'NONE',  ( 1.000000000000000000, 0.000000000000000000, 0.000000000000000000 ) ) ;
#6676=ORIENTED_EDGE ( 'NONE', *, *, #5389, .F. ) ;
#6686=CARTESIAN_POINT ( 'NONE',  ( -2.141980652367355020, -6.189445006155633422, -0.8000000000000000444 ) ) ;
#6695=VECTOR ( 'NONE', #7206, 1000.000000000000000 ) ;
#6721=LINE ( 'NONE', #13493, #10852 ) ;
#6734=DIRECTION ( 'NONE',  ( 1.000000000000000000, 0.000000000000000000, 0.000000000000000000 ) ) ;
#6736=FACE_OUTER_BOUND ( 'NONE', #9719, .T. ) ;
#6748=EDGE_CURVE ( 'NONE', #2957, #5872, #9776, .T. ) ;
#6757=DIRECTION ( 'NONE',  ( 0.000000000000000000, 0.000000000000000000, 1.000000000000000000 ) ) ;
#6760=CARTESIAN_POINT ( 'NONE',  ( -2.321707774797442170, -4.824281976789052351, -0.8000000000000000444 ) ) ;
#6775=DIRECTION ( 'NONE',  ( 0.000000000000000000, 0.000000000000000000, 1.000000000000000000 ) ) ;
#6776=DIRECTION ( 'NONE',  ( 1.000000000000000000, 0.000000000000000000, 0.000000000000000000 ) ) ;
#6794=LINE ( 'NONE', #951, #9945 ) ;
#6801=VECTOR ( 'NONE', #3926, 1000.000000000000000 ) ;
#6805=AXIS2_PLACEMENT_3D ( 'NONE', #1695, #1839, #5237 ) ;
#6807=AXIS2_PLACEMENT_3D ( 'NONE', #7025, #13951, #2196 ) ;
#6829=CIRCLE ( 'NONE', #7082, 4.872650870659752442 ) ;
#6874=ORIENTED_EDGE ( 'NONE', *, *, #2661, .F. ) ;
#6876=CARTESIAN_POINT ( 'NONE',  ( 0.1999999999999985678, -6.997142273814360713, -0.8000000000000000444 ) ) ;
#6883=ORIENTED_EDGE ( 'NONE', *, *, #62, .T. ) ;
#6903=VERTEX_POINT ( 'NONE', #5984 ) ;
#6911=CARTESIAN_POINT ( 'NONE',  ( 1.000000000000000000, -5.408326913195983465, 0.000000000000000000 ) ) ;
#6912=EDGE_CURVE ( 'NONE', #11615, #6129, #7143, .T. ) ;
#6916=ORIENTED_EDGE ( 'NONE', *, *, #914, .T. ) ;
#6920=ADVANCED_FACE ( 'NONE', ( #8288 ), #1293, .T. ) ;
#6986=ORIENTED_EDGE ( 'NONE', *, *, #8379, .T. ) ;
#7025=CARTESIAN_POINT ( 'NONE',  ( 0.9999999999999997780, -6.008326913195983998, -0.8000000000000000444 ) ) ;
#7054=ORIENTED_EDGE ( 'NONE', *, *, #6912, .T. ) ;
#7072=VERTEX_POINT ( 'NONE', #13276 ) ;
#7082=AXIS2_PLACEMENT_3D ( 'NONE', #3649, #7186, #7114 ) ;
#7095=ADVANCED_FACE ( 'NONE', ( #14524 ), #12041, .T. ) ;
#7114=DIRECTION ( 'NONE',  ( 1.000000000000000000, 0.000000000000000000, 0.000000000000000000 ) ) ;
#7121=DIRECTION ( 'NONE',  ( 0.000000000000000000, 0.000000000000000000, 1.000000000000000000 ) ) ;
#7143=LINE ( 'NONE', #3251, #5124 ) ;
#7148=SURFACE_STYLE_USAGE ( .BOTH. , #2465 ) ;
#7163=LINE ( 'NONE', #7242, #10446 ) ;
#7173=ADVANCED_FACE ( 'NONE', ( #10348 ), #5605, .F. ) ;
#7186=DIRECTION ( 'NONE',  ( 0.000000000000000000, 0.000000000000000000, 1.000000000000000000 ) ) ;
#7206=DIRECTION ( 'NONE',  ( -1.000000000000000000, -0.000000000000000000, -0.000000000000000000 ) ) ;
#7242=CARTESIAN_POINT ( 'NONE',  ( -0.1374368770859596967, -4.808326913195983821, -0.8000000000000000444 ) ) ;
#7255=ORIENTED_EDGE ( 'NONE', *, *, #7758, .F. ) ;
#7263=EDGE_LOOP ( 'NONE', ( #14601, #14882, #13075, #3839 ) ) ;
#7275=DIRECTION ( 'NONE',  ( -0.000000000000000000, -0.000000000000000000, -1.000000000000000000 ) ) ;
#7288=CARTESIAN_POINT ( 'NONE',  ( 3.799999999999999378, 0.000000000000000000, -0.8000000000000000444 ) ) ;
#7353=CARTESIAN_POINT ( 'NONE',  ( 0.000000000000000000, 0.000000000000000000, 0.000000000000000000 ) ) ;
#7359=ORIENTED_EDGE ( 'NONE', *, *, #5219, .T. ) ;
#7374=DIRECTION ( 'NONE',  ( -0.000000000000000000, -0.000000000000000000, -1.000000000000000000 ) ) ;
#7388=VERTEX_POINT ( 'NONE', #12948 ) ;
#7417=ORIENTED_EDGE ( 'NONE', *, *, #5979, .T. ) ;
#7431=DIRECTION ( 'NONE',  ( 0.1305261922200521840, 0.9914448613738103822, -0.000000000000000000 ) ) ;
#7459=LINE ( 'NONE', #4157, #6801 ) ;
#7480=CARTESIAN_POINT ( 'NONE',  ( -1.000000000000000000, -6.008326913195983998, -0.8000000000000000444 ) ) ;
#7488=PLANE ( 'NONE',  #8865 ) ;
#7504=ORIENTED_EDGE ( 'NONE', *, *, #8253, .T. ) ;
#7563=DIRECTION ( 'NONE',  ( 0.000000000000000000, 0.000000000000000000, 1.000000000000000000 ) ) ;
#7621=CARTESIAN_POINT ( 'NONE',  ( 1.566204647097437341, -6.822536405429464601, 0.000000000000000000 ) ) ;
#7632=CARTESIAN_POINT ( 'NONE',  ( 1.000000000000000000, -4.808326913195983821, -0.8000000000000000444 ) ) ;
#7645=ORIENTED_EDGE ( 'NONE', *, *, #3259, .F. ) ;
#7666=DIRECTION ( 'NONE',  ( 1.000000000000000000, 0.000000000000000000, -0.000000000000000000 ) ) ;
#7695=ORIENTED_EDGE ( 'NONE', *, *, #6055, .T. ) ;
#7697=EDGE_CURVE ( 'NONE', #5464, #2195, #1033, .T. ) ;
#7704=ORIENTED_EDGE ( 'NONE', *, *, #574, .T. ) ;
#7737=EDGE_CURVE ( 'NONE', #10625, #4617, #10564, .T. ) ;
#7745=DIRECTION ( 'NONE',  ( 1.000000000000000000, 0.000000000000000000, 0.000000000000000000 ) ) ;
#7758=EDGE_CURVE ( 'NONE', #2957, #4474, #9337, .T. ) ;
#7797=CARTESIAN_POINT ( 'NONE',  ( 0.1085714285714285687, -3.798448662927795372, -0.8000000000000000444 ) ) ;
#7799=ORIENTED_EDGE ( 'NONE', *, *, #2526, .F. ) ;
#7820=FACE_OUTER_BOUND ( 'NONE', #2806, .T. ) ;
#7834=VECTOR ( 'NONE', #11496, 1000.000000000000000 ) ;
#7843=CARTESIAN_POINT ( 'NONE',  ( 4.747884751462026820, -5.143694235355983579, -0.8000000000000000444 ) ) ;
#7883=VERTEX_POINT ( 'NONE', #14247 ) ;
#7888=ORIENTED_EDGE ( 'NONE', *, *, #11482, .F. ) ;
#7891=SHAPE_REPRESENTATION ( 'circlip for shafts normal_din_Circlip DIN 471 - 8 x 0.8', ( #1376 ), #3356 ) ;
#7917=AXIS2_PLACEMENT_3D ( 'NONE', #5830, #8344, #13020 ) ;
#7949=VERTEX_POINT ( 'NONE', #14559 ) ;
#7955=EDGE_CURVE ( 'NONE', #8927, #2359, #11135, .T. ) ;
#7986=DIRECTION ( 'NONE',  ( 0.02857142857142857401, -0.9995917534020515305, 0.000000000000000000 ) ) ;
#8019=VECTOR ( 'NONE', #5664, 1000.000000000000000 ) ;
#8047=AXIS2_PLACEMENT_3D ( 'NONE', #4843, #12970, #10319 ) ;
#8059=ORIENTED_EDGE ( 'NONE', *, *, #13418, .F. ) ;
#8075=AXIS2_PLACEMENT_3D ( 'NONE', #11456, #933, #6776 ) ;
#8083=CARTESIAN_POINT ( 'NONE',  ( 0.000000000000000000, 0.000000000000000000, -0.8000000000000000444 ) ) ;
#8109=VERTEX_POINT ( 'NONE', #10909 ) ;
#8122=ORIENTED_EDGE ( 'NONE', *, *, #4652, .T. ) ;
#8125=CARTESIAN_POINT ( 'NONE',  ( -0.2000000000000000111, -6.997142273814360713, 0.000000000000000000 ) ) ;
#8133=DIRECTION ( 'NONE',  ( 0.000000000000000000, 0.000000000000000000, 1.000000000000000000 ) ) ;
#8141=CARTESIAN_POINT ( 'NONE',  ( 0.000000000000000000, 0.000000000000000000, -0.8000000000000000444 ) ) ;
#8142=ORIENTED_EDGE ( 'NONE', *, *, #11623, .F. ) ;
#8143=FILL_AREA_STYLE ('',( #4770 ) ) ;
#8163=LINE ( 'NONE', #14009, #13624 ) ;
#8210=AXIS2_PLACEMENT_3D ( 'NONE', #12889, #10603, #5850 ) ;
#8225=DIRECTION ( 'NONE',  ( -0.000000000000000000, -0.000000000000000000, -1.000000000000000000 ) ) ;
#8248=VECTOR ( 'NONE', #13282, 1000.000000000000114 ) ;
#8253=EDGE_CURVE ( 'NONE', #1577, #6574, #14997, .T. ) ;
#8267=CARTESIAN_POINT ( 'NONE',  ( 2.141980652367355464, -6.189445006155633422, -0.8000000000000000444 ) ) ;
#8270=ORIENTED_EDGE ( 'NONE', *, *, #8533, .T. ) ;
#8272=ADVANCED_FACE ( 'NONE', ( #1927 ), #6617, .T. ) ;
#8280=CARTESIAN_POINT ( 'NONE',  ( 0.000000000000000000, 0.4273491293402468805, 0.000000000000000000 ) ) ;
#8283=CARTESIAN_POINT ( 'NONE',  ( -1.000000000000000222, -4.808326913195983821, -0.8000000000000000444 ) ) ;
#8288=FACE_OUTER_BOUND ( 'NONE', #14664, .T. ) ;
#8298=EDGE_LOOP ( 'NONE', ( #88, #7255, #4568, #5031 ) ) ;
#8315=CYLINDRICAL_SURFACE ( 'NONE', #12151, 2.447112362156698140 ) ;
#8316=CARTESIAN_POINT ( 'NONE',  ( -1.398397006336996817, -6.091550361990593743, -0.8000000000000000444 ) ) ;
#8325=CARTESIAN_POINT ( 'NONE',  ( -4.872650870659752442, 0.4273491293402474911, -0.8000000000000000444 ) ) ;
#8335=CARTESIAN_POINT ( 'NONE',  ( -3.799999999999999378, 4.653657836759941744E-16, -0.8000000000000000444 ) ) ;
#8338=CARTESIAN_POINT ( 'NONE',  ( -1.000000000000000222, -4.808326913195983821, 0.000000000000000000 ) ) ;
#8344=DIRECTION ( 'NONE',  ( 0.000000000000000000, 0.000000000000000000, 1.000000000000000000 ) ) ;
#8347=EDGE_CURVE ( 'NONE', #7388, #3989, #14692, .T. ) ;
#8376=CIRCLE ( 'NONE', #7917, 0.5999999999999998668 ) ;
#8379=EDGE_CURVE ( 'NONE', #10328, #10680, #2003, .T. ) ;
#8455=AXIS2_PLACEMENT_3D ( 'NONE', #8316, #14160, #9616 ) ;
#8463=VERTEX_POINT ( 'NONE', #15219 ) ;
#8484=ADVANCED_FACE ( 'NONE', ( #12013 ), #1496, .T. ) ;
#8499=ORIENTED_EDGE ( 'NONE', *, *, #8533, .F. ) ;
#8508=EDGE_CURVE ( 'NONE', #7883, #12602, #14723, .T. ) ;
#8509=ORIENTED_EDGE ( 'NONE', *, *, #9250, .T. ) ;
#8533=EDGE_CURVE ( 'NONE', #8659, #797, #2816, .T. ) ;
#8557=DIRECTION ( 'NONE',  ( 0.02857142857142857054, -0.9995917534020515305, 0.000000000000000000 ) ) ;
#8609=EDGE_CURVE ( 'NONE', #1278, #9070, #9022, .T. ) ;
#8611=VERTEX_POINT ( 'NONE', #4261 ) ;
#8613=EDGE_CURVE ( 'NONE', #10328, #12415, #5545, .T. ) ;
#8621=LINE ( 'NONE', #7632, #881 ) ;
#8625=EDGE_CURVE ( 'NONE', #3664, #2195, #8163, .T. ) ;
#8642=ORIENTED_EDGE ( 'NONE', *, *, #3647, .T. ) ;
#8655=SHAPE_DEFINITION_REPRESENTATION ( #2954, #7891 ) ;
#8659=VERTEX_POINT ( 'NONE', #10327 ) ;
#8668=DIRECTION ( 'NONE',  ( 1.000000000000000000, -0.000000000000000000, -0.000000000000000000 ) ) ;
#8673=ORIENTED_EDGE ( 'NONE', *, *, #3647, .F. ) ;
#8676=AXIS2_PLACEMENT_3D ( 'NONE', #5881, #12000, #6019 ) ;
#8681=CYLINDRICAL_SURFACE ( 'NONE', #13633, 2.447112362156698140 ) ;
#8697=AXIS2_PLACEMENT_3D ( 'NONE', #10862, #13249, #2730 ) ;
#8732=DIRECTION ( 'NONE',  ( 1.000000000000000000, -0.000000000000000000, -0.000000000000000000 ) ) ;
#8745=ORIENTED_EDGE ( 'NONE', *, *, #9951, .T. ) ;
#8761=AXIS2_PLACEMENT_3D ( 'NONE', #3670, #8133, #4919 ) ;
#8764=CIRCLE ( 'NONE', #2639, 0.5999999999999998668 ) ;
#8788=DIRECTION ( 'NONE',  ( 0.02857142857142857054, 0.9995917534020515305, 0.000000000000000000 ) ) ;
#8790=DIRECTION ( 'NONE',  ( 0.000000000000000000, 0.000000000000000000, 1.000000000000000000 ) ) ;
#8806=ADVANCED_FACE ( 'NONE', ( #1480 ), #14395, .T. ) ;
#8856=ADVANCED_FACE ( 'NONE', ( #13059 ), #2547, .T. ) ;
#8865=AXIS2_PLACEMENT_3D ( 'NONE', #12156, #479, #8557 ) ;
#8877=CIRCLE ( 'NONE', #15028, 7.000000000000000000 ) ;
#8885=PLANE ( 'NONE',  #5892 ) ;
#8927=VERTEX_POINT ( 'NONE', #9920 ) ;
#8955=AXIS2_PLACEMENT_3D ( 'NONE', #15043, #3277, #5670 ) ;
#9009=CIRCLE ( 'NONE', #3127, 4.872650870659752442 ) ;
#9015=ADVANCED_FACE ( 'NONE', ( #11378 ), #5485, .F. ) ;
#9022=LINE ( 'NONE', #721, #11651 ) ;
#9046=CARTESIAN_POINT ( 'NONE',  ( 1.398397006336996817, -6.091550361990593743, -0.8000000000000000444 ) ) ;
#9070=VERTEX_POINT ( 'NONE', #15161 ) ;
#9071=DIRECTION ( 'NONE',  ( -0.000000000000000000, -0.000000000000000000, -1.000000000000000000 ) ) ;
#9148=LINE ( 'NONE', #921, #2120 ) ;
#9183=AXIS2_PLACEMENT_3D ( 'NONE', #11621, #10123, #14818 ) ;
#9194=VECTOR ( 'NONE', #837, 1000.000000000000000 ) ;
#9217=DIRECTION ( 'NONE',  ( 1.000000000000000000, 0.000000000000000000, 0.000000000000000000 ) ) ;
#9250=EDGE_CURVE ( 'NONE', #1278, #2195, #3927, .T. ) ;
#9293=AXIS2_PLACEMENT_3D ( 'NONE', #1980, #3212, #10048 ) ;
#9303=DIRECTION ( 'NONE',  ( -0.000000000000000000, 1.000000000000000000, 0.000000000000000000 ) ) ;
#9308=AXIS2_PLACEMENT_3D ( 'NONE', #9580, #7275, #5057 ) ;
#9320=DIRECTION ( 'NONE',  ( 1.000000000000000000, 0.000000000000000000, 0.000000000000000000 ) ) ;
#9337=LINE ( 'NONE', #11557, #2803 ) ;
#9349=EDGE_CURVE ( 'NONE', #6574, #8927, #5842, .T. ) ;
#9356=EDGE_CURVE ( 'NONE', #797, #7388, #8764, .T. ) ;
#9361=DIRECTION ( 'NONE',  ( 0.000000000000000000, 0.000000000000000000, 1.000000000000000000 ) ) ;
#9363=CARTESIAN_POINT ( 'NONE',  ( -4.872650870659752442, 0.4273491293402474911, 0.000000000000000000 ) ) ;
#9379=CYLINDRICAL_SURFACE ( 'NONE', #10522, 3.799999999999999378 ) ;
#9405=DIRECTION ( 'NONE',  ( 0.000000000000000000, 0.000000000000000000, 1.000000000000000000 ) ) ;
#9417=CARTESIAN_POINT ( 'NONE',  ( 0.000000000000000000, 0.4273491293402468805, -0.8000000000000000444 ) ) ;
#9443=SHAPE_REPRESENTATION_RELATIONSHIP ( 'NONE' , 'NONE' ,  #7891, #675 ) ;
#9464=DIRECTION ( 'NONE',  ( 0.1305261922200521840, 0.9914448613738103822, 0.000000000000000000 ) ) ;
#9507=ORIENTED_EDGE ( 'NONE', *, *, #6468, .F. ) ;
#9516=CARTESIAN_POINT ( 'NONE',  ( 2.141980652367355464, -6.189445006155633422, 0.000000000000000000 ) ) ;
#9530=ORIENTED_EDGE ( 'NONE', *, *, #2526, .T. ) ;
#9538=ORIENTED_EDGE ( 'NONE', *, *, #4574, .F. ) ;
#9559=ORIENTED_EDGE ( 'NONE', *, *, #4687, .T. ) ;
#9580=CARTESIAN_POINT ( 'NONE',  ( 0.000000000000000000, 0.000000000000000000, -0.8000000000000000444 ) ) ;
#9582=EDGE_CURVE ( 'NONE', #8927, #1724, #5913, .T. ) ;
#9614=DIRECTION ( 'NONE',  ( 0.000000000000000000, 0.000000000000000000, 1.000000000000000000 ) ) ;
#9616=DIRECTION ( 'NONE',  ( 1.000000000000000000, 0.000000000000000000, 0.000000000000000000 ) ) ;
#9632=ORIENTED_EDGE ( 'NONE', *, *, #14463, .F. ) ;
#9640=DIRECTION ( 'NONE',  ( 1.000000000000000000, 0.000000000000000000, 0.000000000000000000 ) ) ;
#9685=AXIS2_PLACEMENT_3D ( 'NONE', #1145, #5541, #9217 ) ;
#9719=EDGE_LOOP ( 'NONE', ( #11332, #7504, #13046, #1117 ) ) ;
#9745=ORIENTED_EDGE ( 'NONE', *, *, #12093, .F. ) ;
#9749=ADVANCED_FACE ( 'NONE', ( #9883 ), #1815, .F. ) ;
#9776=CIRCLE ( 'NONE', #12701, 2.447112362156698140 ) ;
#9780=ORIENTED_EDGE ( 'NONE', *, *, #5389, .T. ) ;
#9798=ORIENTED_EDGE ( 'NONE', *, *, #3715, .T. ) ;
#9814=CIRCLE ( 'NONE', #2214, 0.5999999999999999778 ) ;
#9815=ORIENTED_EDGE ( 'NONE', *, *, #2409, .T. ) ;
#9819=CARTESIAN_POINT ( 'NONE',  ( -1.000000000000000000, -5.408326913195983465, -0.8000000000000000444 ) ) ;
#9823=LINE ( 'NONE', #12195, #12073 ) ;
#9836=EDGE_LOOP ( 'NONE', ( #6266, #10919, #14523, #6986 ) ) ;
#9851=CARTESIAN_POINT ( 'NONE',  ( 0.1999999999999985678, -6.997142273814360713, 0.000000000000000000 ) ) ;
#9853=ADVANCED_FACE ( 'NONE', ( #7820 ), #13876, .T. ) ;
#9883=FACE_OUTER_BOUND ( 'NONE', #2648, .T. ) ;
#9897=EDGE_CURVE ( 'NONE', #5629, #5631, #14201, .T. ) ;
#9901=ORIENTED_EDGE ( 'NONE', *, *, #8253, .F. ) ;
#9920=CARTESIAN_POINT ( 'NONE',  ( 1.566204647097437341, -6.822536405429464601, -0.8000000000000000444 ) ) ;
#9945=VECTOR ( 'NONE', #11253, 1000.000000000000000 ) ;
#9950=EDGE_CURVE ( 'NONE', #10680, #7949, #944, .T. ) ;
#9951=EDGE_CURVE ( 'NONE', #7072, #12029, #14185, .T. ) ;
#9975=VERTEX_POINT ( 'NONE', #8335 ) ;
#9980=VECTOR ( 'NONE', #12159, 1000.000000000000114 ) ;
#9981=LINE ( 'NONE', #285, #8248 ) ;
#10000=EDGE_LOOP ( 'NONE', ( #12530, #421, #11543, #7359 ) ) ;
#10013=EDGE_CURVE ( 'NONE', #5631, #4617, #6829, .T. ) ;
#10019=STYLED_ITEM('',(#15272),#14111);
#10035=ORIENTED_EDGE ( 'NONE', *, *, #2192, .T. ) ;
#10043=ORIENTED_EDGE ( 'NONE', *, *, #15201, .T. ) ;
#10048=DIRECTION ( 'NONE',  ( 1.000000000000000000, 0.000000000000000000, 0.000000000000000000 ) ) ;
#10113=VECTOR ( 'NONE', #12350, 1000.000000000000000 ) ;
#10123=DIRECTION ( 'NONE',  ( -0.000000000000000000, -0.000000000000000000, -1.000000000000000000 ) ) ;
#10178=VECTOR ( 'NONE', #7986, 1000.000000000000114 ) ;
#10185=ORIENTED_EDGE ( 'NONE', *, *, #1782, .T. ) ;
#10195=FACE_OUTER_BOUND ( 'NONE', #7263, .T. ) ;
#10199=LINE ( 'NONE', #14896, #4428 ) ;
#10219=CARTESIAN_POINT ( 'NONE',  ( 4.872650870659752442, 0.4273491293402468805, 0.000000000000000000 ) ) ;
#10229=ORIENTED_EDGE ( 'NONE', *, *, #7737, .T. ) ;
#10240=CARTESIAN_POINT ( 'NONE',  ( -1.000000000000000222, -4.808326913195983821, 0.000000000000000000 ) ) ;
#10242=ORIENTED_EDGE ( 'NONE', *, *, #1070, .T. ) ;
#10245=EDGE_CURVE ( 'NONE', #5872, #8109, #12486, .T. ) ;
#10265=ORIENTED_EDGE ( 'NONE', *, *, #14631, .F. ) ;
#10284=EDGE_LOOP ( 'NONE', ( #3775, #1375, #513, #14770 ) ) ;
#10298=ADVANCED_FACE ( 'NONE', ( #10546 ), #9379, .F. ) ;
#10319=DIRECTION ( 'NONE',  ( 0.02857142857142857054, 0.9995917534020515305, 0.000000000000000000 ) ) ;
#10322=ADVANCED_FACE ( 'NONE', ( #2244 ), #2310, .T. ) ;
#10327=CARTESIAN_POINT ( 'NONE',  ( 0.9999999999999997780, -6.008326913195983998, -0.8000000000000000444 ) ) ;
#10328=VERTEX_POINT ( 'NONE', #14302 ) ;
#10334=CARTESIAN_POINT ( 'NONE',  ( -0.1085714285714285687, -3.798448662927795372, -0.8000000000000000444 ) ) ;
#10348=FACE_OUTER_BOUND ( 'NONE', #13126, .T. ) ;
#10375=VECTOR ( 'NONE', #5977, 1000.000000000000000 ) ;
#10377=ORIENTED_EDGE ( 'NONE', *, *, #12208, .F. ) ;
#10405=ORIENTED_EDGE ( 'NONE', *, *, #7697, .T. ) ;
#10431=VECTOR ( 'NONE', #4017, 1000.000000000000000 ) ;
#10446=VECTOR ( 'NONE', #9614, 1000.000000000000000 ) ;
#10456=ORIENTED_EDGE ( 'NONE', *, *, #1931, .F. ) ;
#10464=CIRCLE ( 'NONE', #4091, 2.447112362156698140 ) ;
#10469=( GEOMETRIC_REPRESENTATION_CONTEXT ( 3 ) GLOBAL_UNCERTAINTY_ASSIGNED_CONTEXT ( ( #3015 ) ) GLOBAL_UNIT_ASSIGNED_CONTEXT ( ( #3755, #11820, #3459 ) ) REPRESENTATION_CONTEXT ( 'NONE', 'WORKASPACE' ) );
#10478=ORIENTED_EDGE ( 'NONE', *, *, #7758, .T. ) ;
#10506=CARTESIAN_POINT ( 'NONE',  ( 0.9999999999999997780, -6.008326913195983998, -0.8000000000000000444 ) ) ;
#10522=AXIS2_PLACEMENT_3D ( 'NONE', #3466, #724, #6487 ) ;
#10546=FACE_OUTER_BOUND ( 'NONE', #12248, .T. ) ;
#10564=LINE ( 'NONE', #8325, #3774 ) ;
#10567=FACE_OUTER_BOUND ( 'NONE', #4346, .T. ) ;
#10593=LINE ( 'NONE', #4756, #13179 ) ;
#10603=DIRECTION ( 'NONE',  ( 0.000000000000000000, 0.000000000000000000, 1.000000000000000000 ) ) ;
#10615=CARTESIAN_POINT ( 'NONE',  ( 1.000000000000000000, -6.008326913195983998, 0.000000000000000000 ) ) ;
#10620=AXIS2_PLACEMENT_3D ( 'NONE', #11045, #7374, #6136 ) ;
#10625=VERTEX_POINT ( 'NONE', #4303 ) ;
#10648=CIRCLE ( 'NONE', #3777, 7.000000000000000000 ) ;
#10651=CARTESIAN_POINT ( 'NONE',  ( -0.1717365941144614327, -6.008326913195983998, 0.000000000000000000 ) ) ;
#10665=PLANE ( 'NONE',  #4682 ) ;
#10677=SURFACE_STYLE_FILL_AREA ( #8143 ) ;
#10680=VERTEX_POINT ( 'NONE', #836 ) ;
#10681=ORIENTED_EDGE ( 'NONE', *, *, #2042, .T. ) ;
#10686=EDGE_CURVE ( 'NONE', #10625, #2957, #2556, .T. ) ;
#10704=VECTOR ( 'NONE', #760, 1000.000000000000114 ) ;
#10750=CARTESIAN_POINT ( 'NONE',  ( -1.000000000000000222, -4.808326913195983821, -0.8000000000000000444 ) ) ;
#10754=( GEOMETRIC_REPRESENTATION_CONTEXT ( 3 ) GLOBAL_UNCERTAINTY_ASSIGNED_CONTEXT ( ( #609 ) ) GLOBAL_UNIT_ASSIGNED_CONTEXT ( ( #10866, #1567, #1729 ) ) REPRESENTATION_CONTEXT ( 'NONE', 'WORKASPACE' ) );
#10791=ORIENTED_EDGE ( 'NONE', *, *, #9951, .F. ) ;
#10797=ORIENTED_EDGE ( 'NONE', *, *, #11693, .F. ) ;
#10852=VECTOR ( 'NONE', #11400, 1000.000000000000000 ) ;
#10860=EDGE_LOOP ( 'NONE', ( #2326, #13, #13236, #5837 ) ) ;
#10862=CARTESIAN_POINT ( 'NONE',  ( 0.000000000000000000, 0.4273491293402468805, -0.8000000000000000444 ) ) ;
#10866=( LENGTH_UNIT ( ) NAMED_UNIT ( * ) SI_UNIT ( .MILLI., .METRE. ) );
#10877=CARTESIAN_POINT ( 'NONE',  ( 4.872650870659752442, 0.4273491293402468805, -0.8000000000000000444 ) ) ;
#10882=ORIENTED_EDGE ( 'NONE', *, *, #9582, .T. ) ;
#10909=CARTESIAN_POINT ( 'NONE',  ( -2.321707774797442170, -4.824281976789052351, 0.000000000000000000 ) ) ;
#10919=ORIENTED_EDGE ( 'NONE', *, *, #10245, .F. ) ;
#10925=ORIENTED_EDGE ( 'NONE', *, *, #6468, .T. ) ;
#10971=VERTEX_POINT ( 'NONE', #4213 ) ;
#10972=DIRECTION ( 'NONE',  ( 1.000000000000000000, 0.000000000000000000, 0.000000000000000000 ) ) ;
#10998=CIRCLE ( 'NONE', #12477, 3.799999999999999378 ) ;
#11005=VECTOR ( 'NONE', #9405, 1000.000000000000000 ) ;
#11017=ADVANCED_FACE ( 'NONE', ( #6736 ), #13737, .T. ) ;
#11042=CARTESIAN_POINT ( 'NONE',  ( 2.321707774797442170, -4.824281976789052351, -0.8000000000000000444 ) ) ;
#11045=CARTESIAN_POINT ( 'NONE',  ( 0.000000000000000000, 0.000000000000000000, -0.8000000000000000444 ) ) ;
#11046=PRODUCT ( 'circlip for shafts normal_din_Circlip DIN 471 - 8 x 0.8', 'circlip for shafts normal_din_Circlip DIN 471 - 8 x 0.8', '', ( #6361 ) ) ;
#11074=ORIENTED_EDGE ( 'NONE', *, *, #8609, .F. ) ;
#11085=DIRECTION ( 'NONE',  ( -0.000000000000000000, -0.000000000000000000, -1.000000000000000000 ) ) ;
#11121=CARTESIAN_POINT ( 'NONE',  ( 0.1374368770859596967, -4.808326913195983821, -0.8000000000000000444 ) ) ;
#11131=CLOSED_SHELL ( 'NONE', ( #15026, #8484, #727, #7173, #13235, #6920, #4146, #10298, #12620, #10322, #8806, #8272, #13100, #14633, #12935, #8856, #9853, #7095, #11017, #5978, #15222, #9015, #9749, #716, #5715, #3990, #2499 ) ) ;
#11135=CIRCLE ( 'NONE', #5752, 0.7500000000000002220 ) ;
#11186=ORIENTED_EDGE ( 'NONE', *, *, #7737, .F. ) ;
#11194=MECHANICAL_DESIGN_GEOMETRIC_PRESENTATION_REPRESENTATION('',(#641),#10469);
#11253=DIRECTION ( 'NONE',  ( 0.000000000000000000, 0.000000000000000000, 1.000000000000000000 ) ) ;
#11268=ORIENTED_EDGE ( 'NONE', *, *, #1931, .T. ) ;
#11280=CARTESIAN_POINT ( 'NONE',  ( 0.000000000000000000, 0.000000000000000000, -0.8000000000000000444 ) ) ;
#11290=ORIENTED_EDGE ( 'NONE', *, *, #8609, .T. ) ;
#11304=ORIENTED_EDGE ( 'NONE', *, *, #10686, .F. ) ;
#11332=ORIENTED_EDGE ( 'NONE', *, *, #1782, .F. ) ;
#11364=DIRECTION ( 'NONE',  ( 1.000000000000000000, 0.000000000000000000, 0.000000000000000000 ) ) ;
#11371=DIRECTION ( 'NONE',  ( 0.000000000000000000, 0.000000000000000000, 1.000000000000000000 ) ) ;
#11378=FACE_OUTER_BOUND ( 'NONE', #4750, .T. ) ;
#11387=CIRCLE ( 'NONE', #1327, 3.799999999999999378 ) ;
#11400=DIRECTION ( 'NONE',  ( 0.1305261922200521840, -0.9914448613738103822, 0.000000000000000000 ) ) ;
#11456=CARTESIAN_POINT ( 'NONE',  ( 1.000000000000000000, -5.408326913195983465, -0.8000000000000000444 ) ) ;
#11459=AXIS2_PLACEMENT_3D ( 'NONE', #8083, #12757, #2239 ) ;
#11472=DIRECTION ( 'NONE',  ( 0.000000000000000000, 0.000000000000000000, -1.000000000000000000 ) ) ;
#11482=EDGE_CURVE ( 'NONE', #6574, #12986, #6794, .T. ) ;
#11487=LINE ( 'NONE', #3344, #8019 ) ;
#11496=DIRECTION ( 'NONE',  ( 1.000000000000000000, -0.000000000000000000, -0.000000000000000000 ) ) ;
#11504=AXIS2_PLACEMENT_3D ( 'NONE', #10750, #9303, #5981 ) ;
#11523=CARTESIAN_POINT ( 'NONE',  ( 2.321707774797442170, -4.824281976789052351, -0.8000000000000000444 ) ) ;
#11543=ORIENTED_EDGE ( 'NONE', *, *, #11668, .T. ) ;
#11557=CARTESIAN_POINT ( 'NONE',  ( -3.160591952521660364, -3.281206521718067037, -0.8000000000000000444 ) ) ;
#11586=DIRECTION ( 'NONE',  ( 1.000000000000000000, 0.000000000000000000, 0.000000000000000000 ) ) ;
#11591=DIRECTION ( 'NONE',  ( 0.000000000000000000, -1.000000000000000000, -0.000000000000000000 ) ) ;
#11615=VERTEX_POINT ( 'NONE', #14243 ) ;
#11621=CARTESIAN_POINT ( 'NONE',  ( 0.000000000000000000, 0.000000000000000000, 0.000000000000000000 ) ) ;
#11623=EDGE_CURVE ( 'NONE', #4526, #6903, #13941, .T. ) ;
#11642=CARTESIAN_POINT ( 'NONE',  ( 3.799999999999999378, 0.000000000000000000, 0.000000000000000000 ) ) ;
#11651=VECTOR ( 'NONE', #13713, 1000.000000000000000 ) ;
#11658=DIRECTION ( 'NONE',  ( 1.000000000000000000, 0.000000000000000000, 0.000000000000000000 ) ) ;
#11661=FACE_OUTER_BOUND ( 'NONE', #2837, .T. ) ;
#11668=EDGE_CURVE ( 'NONE', #7388, #5377, #8621, .T. ) ;
#11693=EDGE_CURVE ( 'NONE', #14392, #12029, #14399, .T. ) ;
#11711=CARTESIAN_POINT ( 'NONE',  ( -0.1085714285714285687, -3.798448662927795372, -0.8000000000000000444 ) ) ;
#11750=AXIS2_PLACEMENT_3D ( 'NONE', #13985, #12968, #2372 ) ;
#11773=DIRECTION ( 'NONE',  ( 0.1305261922200521840, 0.9914448613738103822, -0.000000000000000000 ) ) ;
#11777=CARTESIAN_POINT ( 'NONE',  ( -1.000000000000000000, -5.408326913195983465, 0.000000000000000000 ) ) ;
#11816=CARTESIAN_POINT ( 'NONE',  ( -1.566204647097437563, -6.822536405429463713, -0.8000000000000000444 ) ) ;
#11820=( NAMED_UNIT ( * ) PLANE_ANGLE_UNIT ( ) SI_UNIT ( $, .RADIAN. ) );
#11907=ORIENTED_EDGE ( 'NONE', *, *, #12093, .T. ) ;
#11913=EDGE_LOOP ( 'NONE', ( #8270, #12601, #6601, #4744, #14167, #2566, #6145, #5288, #7054, #7417, #8509, #1702, #2322, #3545, #6874, #3549, #11304, #8673, #4564, #10265, #7799, #4931, #13571, #9901, #1462 ) ) ;
#11936=DIRECTION ( 'NONE',  ( 1.000000000000000000, 0.000000000000000000, 0.000000000000000000 ) ) ;
#11953=AXIS2_PLACEMENT_3D ( 'NONE', #4510, #14975, #6734 ) ;
#12000=DIRECTION ( 'NONE',  ( 0.000000000000000000, 0.000000000000000000, 1.000000000000000000 ) ) ;
#12013=FACE_OUTER_BOUND ( 'NONE', #5188, .T. ) ;
#12029=VERTEX_POINT ( 'NONE', #12655 ) ;
#12041=CYLINDRICAL_SURFACE ( 'NONE', #6095, 7.000000000000000000 ) ;
#12073=VECTOR ( 'NONE', #2823, 1000.000000000000000 ) ;
#12086=ORIENTED_EDGE ( 'NONE', *, *, #4695, .F. ) ;
#12091=PLANE ( 'NONE',  #12928 ) ;
#12093=EDGE_CURVE ( 'NONE', #448, #3664, #13587, .T. ) ;
#12128=DIRECTION ( 'NONE',  ( -0.000000000000000000, -0.000000000000000000, -1.000000000000000000 ) ) ;
#12151=AXIS2_PLACEMENT_3D ( 'NONE', #14393, #14706, #1781 ) ;
#12156=CARTESIAN_POINT ( 'NONE',  ( 0.1085714285714285687, -3.798448662927795372, -0.8000000000000000444 ) ) ;
#12159=DIRECTION ( 'NONE',  ( 0.02857142857142857401, -0.9995917534020515305, 0.000000000000000000 ) ) ;
#12181=EDGE_CURVE ( 'NONE', #10971, #12986, #9981, .T. ) ;
#12186=CIRCLE ( 'NONE', #12435, 4.872650870659752442 ) ;
#12195=CARTESIAN_POINT ( 'NONE',  ( -2.321707774797442170, -4.824281976789052351, 0.000000000000000000 ) ) ;
#12208=EDGE_CURVE ( 'NONE', #8463, #3989, #6444, .T. ) ;
#12232=AXIS2_PLACEMENT_3D ( 'NONE', #5783, #4640, #9320 ) ;
#12248=EDGE_LOOP ( 'NONE', ( #964, #7704, #15136, #6676 ) ) ;
#12252=EDGE_LOOP ( 'NONE', ( #10377, #4437, #14426, #2058 ) ) ;
#12277=PRODUCT_DEFINITION ( 'UNKNOWN', '', #14112, #1785 ) ;
#12311=CARTESIAN_POINT ( 'NONE',  ( -4.747884751462026820, -5.143694235355983579, -0.8000000000000000444 ) ) ;
#12323=AXIS2_PLACEMENT_3D ( 'NONE', #6911, #1067, #11658 ) ;
#12325=FACE_OUTER_BOUND ( 'NONE', #13667, .T. ) ;
#12334=LINE ( 'NONE', #10877, #14404 ) ;
#12338=ORIENTED_EDGE ( 'NONE', *, *, #12835, .F. ) ;
#12350=DIRECTION ( 'NONE',  ( 0.000000000000000000, 0.000000000000000000, 1.000000000000000000 ) ) ;
#12415=VERTEX_POINT ( 'NONE', #3441 ) ;
#12435=AXIS2_PLACEMENT_3D ( 'NONE', #9417, #2440, #105 ) ;
#12466=MECHANICAL_DESIGN_GEOMETRIC_PRESENTATION_REPRESENTATION('',(#10019),#10754);
#12477=AXIS2_PLACEMENT_3D ( 'NONE', #600, #12128, #1620 ) ;
#12486=LINE ( 'NONE', #5361, #3639 ) ;
#12496=EDGE_CURVE ( 'NONE', #6903, #5629, #1374, .T. ) ;
#12515=CIRCLE ( 'NONE', #3187, 3.799999999999999378 ) ;
#12517=ORIENTED_EDGE ( 'NONE', *, *, #3715, .F. ) ;
#12530=ORIENTED_EDGE ( 'NONE', *, *, #12208, .T. ) ;
#12532=DIRECTION ( 'NONE',  ( -0.000000000000000000, -0.000000000000000000, -1.000000000000000000 ) ) ;
#12559=ORIENTED_EDGE ( 'NONE', *, *, #14781, .T. ) ;
#12577=EDGE_CURVE ( 'NONE', #7883, #3989, #13551, .T. ) ;
#12601=ORIENTED_EDGE ( 'NONE', *, *, #9356, .T. ) ;
#12602=VERTEX_POINT ( 'NONE', #4188 ) ;
#12620=ADVANCED_FACE ( 'NONE', ( #482 ), #1876, .T. ) ;
#12646=DIRECTION ( 'NONE',  ( 1.000000000000000000, 0.000000000000000000, 0.000000000000000000 ) ) ;
#12655=CARTESIAN_POINT ( 'NONE',  ( -0.1085714285714285687, -3.798448662927795372, 0.000000000000000000 ) ) ;
#12664=DIRECTION ( 'NONE',  ( 0.1305261922200521840, -0.9914448613738103822, 0.000000000000000000 ) ) ;
#12701=AXIS2_PLACEMENT_3D ( 'NONE', #12311, #11085, #6637 ) ;
#12736=ORIENTED_EDGE ( 'NONE', *, *, #914, .F. ) ;
#12757=DIRECTION ( 'NONE',  ( 0.000000000000000000, 0.000000000000000000, 1.000000000000000000 ) ) ;
#12779=DIRECTION ( 'NONE',  ( 0.02857142857142857401, 0.9995917534020515305, -0.000000000000000000 ) ) ;
#12787=DIRECTION ( 'NONE',  ( 0.000000000000000000, 0.000000000000000000, 1.000000000000000000 ) ) ;
#12835=EDGE_CURVE ( 'NONE', #11615, #14392, #7163, .T. ) ;
#12839=ORIENTED_EDGE ( 'NONE', *, *, #14756, .T. ) ;
#12851=CARTESIAN_POINT ( 'NONE',  ( 0.1374368770859597522, -4.808326913195983821, -0.8000000000000000444 ) ) ;
#12860=VECTOR ( 'NONE', #2997, 1000.000000000000000 ) ;
#12866=ORIENTED_EDGE ( 'NONE', *, *, #9250, .F. ) ;
#12889=CARTESIAN_POINT ( 'NONE',  ( 0.000000000000000000, 0.000000000000000000, 0.000000000000000000 ) ) ;
#12892=( NAMED_UNIT ( * ) PLANE_ANGLE_UNIT ( ) SI_UNIT ( $, .RADIAN. ) );
#12915=CIRCLE ( 'NONE', #403, 2.447112362156698140 ) ;
#12928=AXIS2_PLACEMENT_3D ( 'NONE', #13405, #14502, #6117 ) ;
#12935=ADVANCED_FACE ( 'NONE', ( #14312 ), #8315, .F. ) ;
#12948=CARTESIAN_POINT ( 'NONE',  ( 1.000000000000000000, -4.808326913195983821, -0.8000000000000000444 ) ) ;
#12958=AXIS2_PLACEMENT_3D ( 'NONE', #11280, #14981, #7745 ) ;
#12968=DIRECTION ( 'NONE',  ( 0.000000000000000000, 0.000000000000000000, 1.000000000000000000 ) ) ;
#12970=DIRECTION ( 'NONE',  ( 0.9995917534020515305, -0.02857142857142857054, 0.000000000000000000 ) ) ;
#12972=CIRCLE ( 'NONE', #9308, 3.799999999999999378 ) ;
#12974=CARTESIAN_POINT ( 'NONE',  ( 1.599999999999999867, -5.408326913195983465, -0.8000000000000000444 ) ) ;
#12986=VERTEX_POINT ( 'NONE', #9851 ) ;
#13020=DIRECTION ( 'NONE',  ( 1.000000000000000000, 0.000000000000000000, 0.000000000000000000 ) ) ;
#13025=ORIENTED_EDGE ( 'NONE', *, *, #14767, .F. ) ;
#13030=DIRECTION ( 'NONE',  ( 0.000000000000000000, 0.000000000000000000, 1.000000000000000000 ) ) ;
#13046=ORIENTED_EDGE ( 'NONE', *, *, #11482, .T. ) ;
#13059=FACE_OUTER_BOUND ( 'NONE', #1087, .T. ) ;
#13075=ORIENTED_EDGE ( 'NONE', *, *, #4574, .T. ) ;
#13092=PLANE ( 'NONE',  #1030 ) ;
#13100=ADVANCED_FACE ( 'NONE', ( #5186 ), #8681, .F. ) ;
#13124=( LENGTH_UNIT ( ) NAMED_UNIT ( * ) SI_UNIT ( .MILLI., .METRE. ) );
#13126=EDGE_LOOP ( 'NONE', ( #13618, #6916, #14192, #10791 ) ) ;
#13131=VECTOR ( 'NONE', #12779, 1000.000000000000114 ) ;
#13179=VECTOR ( 'NONE', #272, 1000.000000000000114 ) ;
#13186=ORIENTED_EDGE ( 'NONE', *, *, #7955, .T. ) ;
#13235=ADVANCED_FACE ( 'NONE', ( #3395 ), #5484, .F. ) ;
#13236=ORIENTED_EDGE ( 'NONE', *, *, #14631, .T. ) ;
#13249=DIRECTION ( 'NONE',  ( 0.000000000000000000, 0.000000000000000000, 1.000000000000000000 ) ) ;
#13260=LINE ( 'NONE', #5287, #2260 ) ;
#13263=ORIENTED_EDGE ( 'NONE', *, *, #9582, .F. ) ;
#13276=CARTESIAN_POINT ( 'NONE',  ( -0.1085714285714285687, -3.798448662927795372, -0.8000000000000000444 ) ) ;
#13282=DIRECTION ( 'NONE',  ( 0.02857142857142857401, -0.9995917534020515305, 0.000000000000000000 ) ) ;
#13309=LINE ( 'NONE', #1789, #10431 ) ;
#13314=FACE_OUTER_BOUND ( 'NONE', #12252, .T. ) ;
#13391=CARTESIAN_POINT ( 'NONE',  ( -3.799999999999999378, 4.653657836759941744E-16, 0.000000000000000000 ) ) ;
#13398=ORIENTED_EDGE ( 'NONE', *, *, #4695, .T. ) ;
#13405=CARTESIAN_POINT ( 'NONE',  ( 0.000000000000000000, 0.000000000000000000, 0.000000000000000000 ) ) ;
#13418=EDGE_CURVE ( 'NONE', #2359, #4526, #7459, .T. ) ;
#13441=VERTEX_POINT ( 'NONE', #5171 ) ;
#13451=ORIENTED_EDGE ( 'NONE', *, *, #3259, .T. ) ;
#13481=DIRECTION ( 'NONE',  ( 1.000000000000000000, 0.000000000000000000, 0.000000000000000000 ) ) ;
#13483=ORIENTED_EDGE ( 'NONE', *, *, #10013, .T. ) ;
#13493=CARTESIAN_POINT ( 'NONE',  ( -2.321707774797442170, -4.824281976789052351, -0.8000000000000000444 ) ) ;
#13504=DIRECTION ( 'NONE',  ( 0.000000000000000000, 0.000000000000000000, 1.000000000000000000 ) ) ;
#13523=ORIENTED_EDGE ( 'NONE', *, *, #6055, .F. ) ;
#13551=LINE ( 'NONE', #2953, #9980 ) ;
#13571=ORIENTED_EDGE ( 'NONE', *, *, #9349, .F. ) ;
#13579=DIRECTION ( 'NONE',  ( 1.000000000000000000, 0.000000000000000000, 0.000000000000000000 ) ) ;
#13587=LINE ( 'NONE', #6609, #10704 ) ;
#13618=ORIENTED_EDGE ( 'NONE', *, *, #3133, .T. ) ;
#13624=VECTOR ( 'NONE', #11472, 1000.000000000000000 ) ;
#13633=AXIS2_PLACEMENT_3D ( 'NONE', #15008, #6775, #3094 ) ;
#13660=CARTESIAN_POINT ( 'NONE',  ( -0.2000000000000000111, -6.997142273814360713, -0.8000000000000000444 ) ) ;
#13667=EDGE_LOOP ( 'NONE', ( #4318, #9538, #3005, #14221, #1522, #13451, #2956, #568, #3553, #1836, #13483, #12559, #10681, #6515, #14627, #5495, #11907, #12086, #9507, #1687, #4880, #2484, #10, #9780, #12839 ) ) ;
#13713=DIRECTION ( 'NONE',  ( -0.000000000000000000, -0.000000000000000000, 1.000000000000000000 ) ) ;
#13737=PLANE ( 'NONE',  #8955 ) ;
#13754=DIRECTION ( 'NONE',  ( 0.000000000000000000, 0.000000000000000000, 1.000000000000000000 ) ) ;
#13833=ORIENTED_EDGE ( 'NONE', *, *, #2392, .F. ) ;
#13841=DIRECTION ( 'NONE',  ( -1.000000000000000000, -0.000000000000000000, -0.000000000000000000 ) ) ;
#13860=AXIS2_PLACEMENT_3D ( 'NONE', #6760, #3299, #12664 ) ;
#13876=CYLINDRICAL_SURFACE ( 'NONE', #6333, 0.7500000000000002220 ) ;
#13901=CYLINDRICAL_SURFACE ( 'NONE', #4108, 4.872650870659752442 ) ;
#13941=LINE ( 'NONE', #5879, #1853 ) ;
#13951=DIRECTION ( 'NONE',  ( 0.000000000000000000, -1.000000000000000000, -0.000000000000000000 ) ) ;
#13975=DIRECTION ( 'NONE',  ( -0.000000000000000000, -0.000000000000000000, -1.000000000000000000 ) ) ;
#13985=CARTESIAN_POINT ( 'NONE',  ( 0.000000000000000000, 0.4273491293402468805, -0.8000000000000000444 ) ) ;
#14009=CARTESIAN_POINT ( 'NONE',  ( -0.1717365941144614605, -6.008326913195983998, -0.8000000000000000444 ) ) ;
#14020=ORIENTED_EDGE ( 'NONE', *, *, #8625, .T. ) ;
#14024=EDGE_LOOP ( 'NONE', ( #11186, #5921, #10478, #2564 ) ) ;
#14048=VECTOR ( 'NONE', #8732, 1000.000000000000000 ) ;
#14090=DIRECTION ( 'NONE',  ( 0.000000000000000000, 0.000000000000000000, 1.000000000000000000 ) ) ;
#14103=VECTOR ( 'NONE', #1726, 1000.000000000000000 ) ;
#14111=MANIFOLD_SOLID_BREP ( 'Notch', #11131 ) ;
#14112=PRODUCT_DEFINITION_FORMATION_WITH_SPECIFIED_SOURCE ( 'ANY', '', #11046, .NOT_KNOWN. ) ;
#14160=DIRECTION ( 'NONE',  ( 0.000000000000000000, 0.000000000000000000, 1.000000000000000000 ) ) ;
#14167=ORIENTED_EDGE ( 'NONE', *, *, #574, .F. ) ;
#14185=LINE ( 'NONE', #11711, #11005 ) ;
#14192=ORIENTED_EDGE ( 'NONE', *, *, #932, .F. ) ;
#14201=CIRCLE ( 'NONE', #9293, 4.872650870659752442 ) ;
#14221=ORIENTED_EDGE ( 'NONE', *, *, #1254, .F. ) ;
#14236=VECTOR ( 'NONE', #121, 1000.000000000000000 ) ;
#14243=CARTESIAN_POINT ( 'NONE',  ( -0.1374368770859597522, -4.808326913195983821, -0.8000000000000000444 ) ) ;
#14247=CARTESIAN_POINT ( 'NONE',  ( 0.1085714285714285687, -3.798448662927795372, -0.8000000000000000444 ) ) ;
#14254=CARTESIAN_POINT ( 'NONE',  ( 4.747884751462026820, -5.143694235355983579, 0.000000000000000000 ) ) ;
#14279=DIRECTION ( 'NONE',  ( 1.000000000000000000, 0.000000000000000000, 0.000000000000000000 ) ) ;
#14294=ORIENTED_EDGE ( 'NONE', *, *, #2192, .F. ) ;
#14302=CARTESIAN_POINT ( 'NONE',  ( -2.141980652367355020, -6.189445006155633422, -0.8000000000000000444 ) ) ;
#14312=FACE_OUTER_BOUND ( 'NONE', #10860, .T. ) ;
#14392=VERTEX_POINT ( 'NONE', #6379 ) ;
#14393=CARTESIAN_POINT ( 'NONE',  ( 4.747884751462026820, -5.143694235355983579, -0.8000000000000000444 ) ) ;
#14395=CYLINDRICAL_SURFACE ( 'NONE', #8455, 0.7500000000000002220 ) ;
#14397=EDGE_LOOP ( 'NONE', ( #13833, #10456, #4291, #10035 ) ) ;
#14399=LINE ( 'NONE', #3867, #3577 ) ;
#14404=VECTOR ( 'NONE', #14659, 1000.000000000000000 ) ;
#14426=ORIENTED_EDGE ( 'NONE', *, *, #8508, .F. ) ;
#14428=CARTESIAN_POINT ( 'NONE',  ( -1.000000000000000222, -4.808326913195983821, -0.8000000000000000444 ) ) ;
#14463=EDGE_CURVE ( 'NONE', #4099, #5041, #10998, .T. ) ;
#14502=DIRECTION ( 'NONE',  ( 0.000000000000000000, 0.000000000000000000, 1.000000000000000000 ) ) ;
#14514=DIRECTION ( 'NONE',  ( 1.000000000000000000, 0.000000000000000000, 0.000000000000000000 ) ) ;
#14523=ORIENTED_EDGE ( 'NONE', *, *, #2661, .T. ) ;
#14524=FACE_OUTER_BOUND ( 'NONE', #651, .T. ) ;
#14559=CARTESIAN_POINT ( 'NONE',  ( -1.566204647097437563, -6.822536405429463713, 0.000000000000000000 ) ) ;
#14601=ORIENTED_EDGE ( 'NONE', *, *, #9356, .F. ) ;
#14627=ORIENTED_EDGE ( 'NONE', *, *, #9950, .T. ) ;
#14631=EDGE_CURVE ( 'NONE', #3152, #13441, #12915, .T. ) ;
#14633=ADVANCED_FACE ( 'NONE', ( #5689 ), #13901, .T. ) ;
#14654=EDGE_LOOP ( 'NONE', ( #4839, #9745, #14294, #10405 ) ) ;
#14659=DIRECTION ( 'NONE',  ( 0.000000000000000000, 0.000000000000000000, 1.000000000000000000 ) ) ;
#14664=EDGE_LOOP ( 'NONE', ( #12338, #10043, #8745, #10797 ) ) ;
#14692=LINE ( 'NONE', #14917, #12860 ) ;
#14706=DIRECTION ( 'NONE',  ( 0.000000000000000000, 0.000000000000000000, 1.000000000000000000 ) ) ;
#14723=LINE ( 'NONE', #7797, #14103 ) ;
#14750=CARTESIAN_POINT ( 'NONE',  ( 0.000000000000000000, 0.000000000000000000, -0.8000000000000000444 ) ) ;
#14756=EDGE_CURVE ( 'NONE', #12602, #8463, #10593, .T. ) ;
#14767=EDGE_CURVE ( 'NONE', #1724, #4526, #156, .T. ) ;
#14770=ORIENTED_EDGE ( 'NONE', *, *, #6912, .F. ) ;
#14781=EDGE_CURVE ( 'NONE', #4617, #4474, #9009, .T. ) ;
#14818=DIRECTION ( 'NONE',  ( 1.000000000000000000, 0.000000000000000000, 0.000000000000000000 ) ) ;
#14882=ORIENTED_EDGE ( 'NONE', *, *, #3274, .T. ) ;
#14896=CARTESIAN_POINT ( 'NONE',  ( 0.9999999999999997780, -6.008326913195983998, -0.8000000000000000444 ) ) ;
#14917=CARTESIAN_POINT ( 'NONE',  ( -1.000000000000000222, -4.808326913195983821, -0.8000000000000000444 ) ) ;
#14923=EDGE_CURVE ( 'NONE', #3152, #6903, #427, .T. ) ;
#14974=DIRECTION ( 'NONE',  ( 1.000000000000000000, 0.000000000000000000, 0.000000000000000000 ) ) ;
#14975=DIRECTION ( 'NONE',  ( 0.000000000000000000, 0.000000000000000000, 1.000000000000000000 ) ) ;
#14981=DIRECTION ( 'NONE',  ( 0.000000000000000000, 0.000000000000000000, 1.000000000000000000 ) ) ;
#14997=LINE ( 'NONE', #1843, #10178 ) ;
#15008=CARTESIAN_POINT ( 'NONE',  ( -4.747884751462026820, -5.143694235355983579, -0.8000000000000000444 ) ) ;
#15026=ADVANCED_FACE ( 'NONE', ( #10195 ), #1045, .F. ) ;
#15028=AXIS2_PLACEMENT_3D ( 'NONE', #1272, #7121, #5965 ) ;
#15043=CARTESIAN_POINT ( 'NONE',  ( 0.1085714285714285687, -3.798448662927795372, -0.8000000000000000444 ) ) ;
#15110=VERTEX_POINT ( 'NONE', #8338 ) ;
#15136=ORIENTED_EDGE ( 'NONE', *, *, #8508, .T. ) ;
#15146=CYLINDRICAL_SURFACE ( 'NONE', #11750, 4.872650870659752442 ) ;
#15161=CARTESIAN_POINT ( 'NONE',  ( -1.000000000000000000, -6.008326913195983998, 0.000000000000000000 ) ) ;
#15201=EDGE_CURVE ( 'NONE', #11615, #7072, #25, .T. ) ;
#15219=CARTESIAN_POINT ( 'NONE',  ( 0.1374368770859597522, -4.808326913195983821, 0.000000000000000000 ) ) ;
#15222=ADVANCED_FACE ( 'NONE', ( #12325 ), #12091, .T. ) ;
#15266=COLOUR_RGB('Grey',0.48,0.52,0.57);
#15267=FILL_AREA_STYLE_COLOUR('',#15266);
#15268=FILL_AREA_STYLE('',(#15267));
#15269=SURFACE_STYLE_FILL_AREA(#15268);
#15270=SURFACE_SIDE_STYLE('',(#15269));
#15271=SURFACE_STYLE_USAGE(.BOTH.,#15270);
#15272=PRESENTATION_STYLE_ASSIGNMENT((#15271));
ENDSEC;
END-ISO-10303-21;
